ISO-10303-21;
HEADER;
/* Generated by software containing ST-Developer
 * from STEP Tools, Inc. (www.steptools.com) 
 */

FILE_DESCRIPTION(
/* description */ (''),
/* implementation_level */ '2;1');

FILE_NAME(
/* name */ 'Top_Block.step',
/* time_stamp */ '2026-10-23T22:30:33+06:00',
/* author */ (''),
/* organization */ (''),
/* preprocessor_version */ 'ST-DEVELOPER v20.2',
/* originating_system */ 'Autodesk Translation Framework v15.15.0.0',
/* authorisation */ '');

FILE_SCHEMA (('AUTOMOTIVE_DESIGN { 1 0 10303 214 3 1 1 }'));
ENDSEC;

DATA;
#10=MECHANICAL_DESIGN_GEOMETRIC_PRESENTATION_REPRESENTATION('',(#237),#10131);
#51=ELLIPSE('',#6109,1.08239220029239,1.);
#52=ELLIPSE('',#6111,1.08239220029239,1.);
#53=ELLIPSE('',#6115,1.08239220029239,1.);
#54=ELLIPSE('',#6117,1.08239220029239,1.);
#55=ELLIPSE('',#6119,1.0823922002924,1.);
#56=ELLIPSE('',#6120,1.08239220029239,1.);
#57=ELLIPSE('',#6122,1.08239220029239,1.);
#58=ELLIPSE('',#6123,1.0823922002924,1.);
#59=ELLIPSE('',#6125,1.0823922002924,1.);
#60=ELLIPSE('',#6127,1.0823922002924,1.);
#61=ELLIPSE('',#6128,1.0823922002924,1.);
#62=ELLIPSE('',#6130,1.08239220029239,1.);
#63=ELLIPSE('',#6133,1.08239220029239,1.);
#64=ELLIPSE('',#6135,1.0823922002924,1.);
#65=ELLIPSE('',#6138,1.08239220029239,1.);
#66=ELLIPSE('',#6140,1.0823922002924,1.);
#67=ELLIPSE('',#6150,1.08239220029239,1.);
#68=ELLIPSE('',#6152,1.08239220029239,1.);
#69=ELLIPSE('',#6155,1.08239220029239,1.);
#70=ELLIPSE('',#6157,1.0823922002924,1.);
#71=ELLIPSE('',#6159,1.08239220029239,1.);
#72=ELLIPSE('',#6161,1.08239220029239,1.);
#73=ELLIPSE('',#6163,1.0823922002924,1.);
#74=ELLIPSE('',#6165,1.0823922002924,1.);
#207=B_SPLINE_CURVE_WITH_KNOTS('',3,(#8653,#8654,#8655,#8656,#8657,#8658,
#8659,#8660,#8661,#8662),.UNSPECIFIED.,.F.,.F.,(4,2,2,2,4),(0.,0.179989683878213,
0.359979367756426,0.499959890996325,0.633875417351683),.UNSPECIFIED.);
#208=B_SPLINE_CURVE_WITH_KNOTS('',3,(#8673,#8674,#8675,#8676,#8677,#8678,
#8679,#8680,#8681,#8682),.UNSPECIFIED.,.F.,.F.,(4,2,2,2,4),(1.82590429893059,
1.95981982528595,2.09980034852585,2.27979003240406,2.45977971628227),
 .UNSPECIFIED.);
#209=B_SPLINE_CURVE_WITH_KNOTS('',3,(#8698,#8699,#8700,#8701,#8702,#8703,
#8704,#8705,#8706,#8707),.UNSPECIFIED.,.F.,.F.,(4,2,2,2,4),(0.,0.179989683878213,
0.359979367756426,0.499959890996325,0.633875417351683),.UNSPECIFIED.);
#210=B_SPLINE_CURVE_WITH_KNOTS('',3,(#8718,#8719,#8720,#8721,#8722,#8723,
#8724,#8725,#8726,#8727),.UNSPECIFIED.,.F.,.F.,(4,2,2,2,4),(1.82590429893059,
1.95981982528595,2.09980034852585,2.27979003240406,2.45977971628227),
 .UNSPECIFIED.);
#211=TOROIDAL_SURFACE('',#6075,5.,4.);
#212=TOROIDAL_SURFACE('',#6081,5.,4.);
#213=TOROIDAL_SURFACE('',#6085,5.,4.);
#214=TOROIDAL_SURFACE('',#6091,5.,4.);
#217=SHAPE_REPRESENTATION_RELATIONSHIP('SRR','None',#10171,#227);
#227=ADVANCED_BREP_SHAPE_REPRESENTATION('',(#247),#10123);
#237=STYLED_ITEM('',(#10247),#247);
#247=MANIFOLD_SOLID_BREP('Top_Block',#5881);
#273=FACE_BOUND('',#895,.T.);
#274=FACE_BOUND('',#896,.T.);
#275=FACE_BOUND('',#898,.T.);
#276=FACE_BOUND('',#899,.T.);
#277=FACE_BOUND('',#921,.T.);
#278=FACE_BOUND('',#922,.T.);
#279=FACE_BOUND('',#923,.T.);
#280=FACE_BOUND('',#924,.T.);
#356=PLANE('',#6084);
#357=PLANE('',#6094);
#358=PLANE('',#6107);
#359=PLANE('',#6112);
#360=PLANE('',#6113);
#361=PLANE('',#6142);
#362=PLANE('',#6143);
#363=PLANE('',#6144);
#364=PLANE('',#6145);
#365=PLANE('',#6146);
#366=PLANE('',#6147);
#367=PLANE('',#6148);
#368=PLANE('',#6167);
#369=PLANE('',#6168);
#370=PLANE('',#6169);
#371=PLANE('',#6170);
#372=PLANE('',#6171);
#373=PLANE('',#6172);
#512=FACE_OUTER_BOUND('',#879,.T.);
#513=FACE_OUTER_BOUND('',#880,.T.);
#514=FACE_OUTER_BOUND('',#881,.T.);
#515=FACE_OUTER_BOUND('',#882,.T.);
#516=FACE_OUTER_BOUND('',#883,.T.);
#517=FACE_OUTER_BOUND('',#884,.T.);
#518=FACE_OUTER_BOUND('',#885,.T.);
#519=FACE_OUTER_BOUND('',#886,.T.);
#520=FACE_OUTER_BOUND('',#887,.T.);
#521=FACE_OUTER_BOUND('',#888,.T.);
#522=FACE_OUTER_BOUND('',#889,.T.);
#523=FACE_OUTER_BOUND('',#890,.T.);
#524=FACE_OUTER_BOUND('',#891,.T.);
#525=FACE_OUTER_BOUND('',#892,.T.);
#526=FACE_OUTER_BOUND('',#893,.T.);
#527=FACE_OUTER_BOUND('',#894,.T.);
#528=FACE_OUTER_BOUND('',#897,.T.);
#529=FACE_OUTER_BOUND('',#900,.T.);
#530=FACE_OUTER_BOUND('',#901,.T.);
#531=FACE_OUTER_BOUND('',#902,.T.);
#532=FACE_OUTER_BOUND('',#903,.T.);
#533=FACE_OUTER_BOUND('',#904,.T.);
#534=FACE_OUTER_BOUND('',#905,.T.);
#535=FACE_OUTER_BOUND('',#906,.T.);
#536=FACE_OUTER_BOUND('',#907,.T.);
#537=FACE_OUTER_BOUND('',#908,.T.);
#538=FACE_OUTER_BOUND('',#909,.T.);
#539=FACE_OUTER_BOUND('',#910,.T.);
#540=FACE_OUTER_BOUND('',#911,.T.);
#541=FACE_OUTER_BOUND('',#912,.T.);
#542=FACE_OUTER_BOUND('',#913,.T.);
#543=FACE_OUTER_BOUND('',#914,.T.);
#544=FACE_OUTER_BOUND('',#915,.T.);
#545=FACE_OUTER_BOUND('',#916,.T.);
#546=FACE_OUTER_BOUND('',#917,.T.);
#547=FACE_OUTER_BOUND('',#918,.T.);
#548=FACE_OUTER_BOUND('',#919,.T.);
#549=FACE_OUTER_BOUND('',#920,.T.);
#550=FACE_OUTER_BOUND('',#925,.T.);
#551=FACE_OUTER_BOUND('',#926,.T.);
#552=FACE_OUTER_BOUND('',#927,.T.);
#553=FACE_OUTER_BOUND('',#928,.T.);
#554=FACE_OUTER_BOUND('',#929,.T.);
#555=FACE_OUTER_BOUND('',#930,.T.);
#556=FACE_OUTER_BOUND('',#931,.T.);
#557=FACE_OUTER_BOUND('',#932,.T.);
#558=FACE_OUTER_BOUND('',#933,.T.);
#559=FACE_OUTER_BOUND('',#934,.T.);
#560=FACE_OUTER_BOUND('',#935,.T.);
#561=FACE_OUTER_BOUND('',#936,.T.);
#562=FACE_OUTER_BOUND('',#937,.T.);
#563=FACE_OUTER_BOUND('',#938,.T.);
#564=FACE_OUTER_BOUND('',#939,.T.);
#565=FACE_OUTER_BOUND('',#940,.T.);
#879=EDGE_LOOP('',(#3938,#3939,#3940,#3941));
#880=EDGE_LOOP('',(#3942,#3943,#3944,#3945));
#881=EDGE_LOOP('',(#3946,#3947,#3948,#3949));
#882=EDGE_LOOP('',(#3950,#3951,#3952,#3953,#3954,#3955));
#883=EDGE_LOOP('',(#3956,#3957,#3958,#3959));
#884=EDGE_LOOP('',(#3960,#3961,#3962,#3963));
#885=EDGE_LOOP('',(#3964,#3965,#3966,#3967));
#886=EDGE_LOOP('',(#3968,#3969,#3970,#3971,#3972,#3973));
#887=EDGE_LOOP('',(#3974,#3975,#3976,#3977));
#888=EDGE_LOOP('',(#3978,#3979,#3980,#3981));
#889=EDGE_LOOP('',(#3982,#3983,#3984,#3985));
#890=EDGE_LOOP('',(#3986,#3987,#3988,#3989));
#891=EDGE_LOOP('',(#3990,#3991,#3992,#3993));
#892=EDGE_LOOP('',(#3994,#3995,#3996,#3997));
#893=EDGE_LOOP('',(#3998,#3999,#4000,#4001));
#894=EDGE_LOOP('',(#4002,#4003,#4004,#4005,#4006,#4007));
#895=EDGE_LOOP('',(#4008));
#896=EDGE_LOOP('',(#4009));
#897=EDGE_LOOP('',(#4010,#4011,#4012,#4013,#4014,#4015,#4016,#4017,#4018,
#4019));
#898=EDGE_LOOP('',(#4020));
#899=EDGE_LOOP('',(#4021));
#900=EDGE_LOOP('',(#4022,#4023,#4024,#4025));
#901=EDGE_LOOP('',(#4026,#4027,#4028,#4029));
#902=EDGE_LOOP('',(#4030,#4031,#4032,#4033));
#903=EDGE_LOOP('',(#4034,#4035,#4036,#4037));
#904=EDGE_LOOP('',(#4038,#4039,#4040,#4041));
#905=EDGE_LOOP('',(#4042,#4043,#4044,#4045));
#906=EDGE_LOOP('',(#4046,#4047,#4048,#4049));
#907=EDGE_LOOP('',(#4050,#4051,#4052,#4053));
#908=EDGE_LOOP('',(#4054,#4055,#4056,#4057));
#909=EDGE_LOOP('',(#4058,#4059,#4060,#4061));
#910=EDGE_LOOP('',(#4062,#4063,#4064,#4065));
#911=EDGE_LOOP('',(#4066,#4067,#4068,#4069));
#912=EDGE_LOOP('',(#4070,#4071,#4072,#4073));
#913=EDGE_LOOP('',(#4074,#4075,#4076,#4077));
#914=EDGE_LOOP('',(#4078,#4079,#4080,#4081));
#915=EDGE_LOOP('',(#4082,#4083,#4084,#4085));
#916=EDGE_LOOP('',(#4086,#4087,#4088,#4089));
#917=EDGE_LOOP('',(#4090,#4091,#4092,#4093));
#918=EDGE_LOOP('',(#4094,#4095,#4096,#4097));
#919=EDGE_LOOP('',(#4098,#4099,#4100,#4101));
#920=EDGE_LOOP('',(#4102,#4103,#4104,#4105,#4106,#4107,#4108,#4109,#4110,
#4111,#4112,#4113));
#921=EDGE_LOOP('',(#4114));
#922=EDGE_LOOP('',(#4115));
#923=EDGE_LOOP('',(#4116));
#924=EDGE_LOOP('',(#4117));
#925=EDGE_LOOP('',(#4118,#4119,#4120,#4121));
#926=EDGE_LOOP('',(#4122,#4123,#4124,#4125));
#927=EDGE_LOOP('',(#4126,#4127,#4128,#4129));
#928=EDGE_LOOP('',(#4130,#4131,#4132,#4133));
#929=EDGE_LOOP('',(#4134,#4135,#4136,#4137));
#930=EDGE_LOOP('',(#4138,#4139,#4140,#4141));
#931=EDGE_LOOP('',(#4142,#4143,#4144,#4145));
#932=EDGE_LOOP('',(#4146,#4147,#4148,#4149));
#933=EDGE_LOOP('',(#4150,#4151,#4152,#4153));
#934=EDGE_LOOP('',(#4154,#4155,#4156,#4157));
#935=EDGE_LOOP('',(#4158,#4159,#4160,#4161,#4162,#4163,#4164,#4165,#4166,
#4167));
#936=EDGE_LOOP('',(#4168,#4169,#4170,#4171));
#937=EDGE_LOOP('',(#4172,#4173,#4174,#4175));
#938=EDGE_LOOP('',(#4176,#4177,#4178,#4179));
#939=EDGE_LOOP('',(#4180,#4181,#4182,#4183,#4184,#4185,#4186,#4187,#4188,
#4189));
#940=EDGE_LOOP('',(#4190,#4191,#4192,#4193));
#1319=LINE('',#8668,#1869);
#1320=LINE('',#8669,#1870);
#1321=LINE('',#8687,#1871);
#1322=LINE('',#8689,#1872);
#1323=LINE('',#8690,#1873);
#1324=LINE('',#8713,#1874);
#1325=LINE('',#8714,#1875);
#1326=LINE('',#8732,#1876);
#1327=LINE('',#8734,#1877);
#1328=LINE('',#8735,#1878);
#1329=LINE('',#8740,#1879);
#1330=LINE('',#8746,#1880);
#1331=LINE('',#8752,#1881);
#1332=LINE('',#8758,#1882);
#1333=LINE('',#8761,#1883);
#1334=LINE('',#8762,#1884);
#1335=LINE('',#8765,#1885);
#1336=LINE('',#8768,#1886);
#1337=LINE('',#8771,#1887);
#1338=LINE('',#8774,#1888);
#1339=LINE('',#8777,#1889);
#1340=LINE('',#8779,#1890);
#1341=LINE('',#8781,#1891);
#1342=LINE('',#8782,#1892);
#1343=LINE('',#8785,#1893);
#1344=LINE('',#8787,#1894);
#1345=LINE('',#8789,#1895);
#1346=LINE('',#8791,#1896);
#1347=LINE('',#8793,#1897);
#1348=LINE('',#8795,#1898);
#1349=LINE('',#8797,#1899);
#1350=LINE('',#8798,#1900);
#1351=LINE('',#8802,#1901);
#1352=LINE('',#8805,#1902);
#1353=LINE('',#8810,#1903);
#1354=LINE('',#8814,#1904);
#1355=LINE('',#8819,#1905);
#1356=LINE('',#8823,#1906);
#1357=LINE('',#8827,#1907);
#1358=LINE('',#8830,#1908);
#1359=LINE('',#8834,#1909);
#1360=LINE('',#8838,#1910);
#1361=LINE('',#8842,#1911);
#1362=LINE('',#8845,#1912);
#1363=LINE('',#8847,#1913);
#1364=LINE('',#8848,#1914);
#1365=LINE('',#8851,#1915);
#1366=LINE('',#8853,#1916);
#1367=LINE('',#8857,#1917);
#1368=LINE('',#8859,#1918);
#1369=LINE('',#8862,#1919);
#1370=LINE('',#8863,#1920);
#1371=LINE('',#8866,#1921);
#1372=LINE('',#8868,#1922);
#1373=LINE('',#8872,#1923);
#1374=LINE('',#8874,#1924);
#1375=LINE('',#8877,#1925);
#1376=LINE('',#8878,#1926);
#1377=LINE('',#8881,#1927);
#1378=LINE('',#8882,#1928);
#1379=LINE('',#8883,#1929);
#1380=LINE('',#8886,#1930);
#1381=LINE('',#8887,#1931);
#1382=LINE('',#8890,#1932);
#1383=LINE('',#8891,#1933);
#1384=LINE('',#8894,#1934);
#1385=LINE('',#8895,#1935);
#1386=LINE('',#8898,#1936);
#1387=LINE('',#8899,#1937);
#1388=LINE('',#8902,#1938);
#1389=LINE('',#8903,#1939);
#1390=LINE('',#8908,#1940);
#1391=LINE('',#8912,#1941);
#1392=LINE('',#8914,#1942);
#1393=LINE('',#8917,#1943);
#1394=LINE('',#8930,#1944);
#1395=LINE('',#8932,#1945);
#1396=LINE('',#8934,#1946);
#1397=LINE('',#8936,#1947);
#1398=LINE('',#8938,#1948);
#1869=VECTOR('',#6869,10.);
#1870=VECTOR('',#6870,10.);
#1871=VECTOR('',#6879,10.);
#1872=VECTOR('',#6880,10.);
#1873=VECTOR('',#6881,10.);
#1874=VECTOR('',#6894,10.);
#1875=VECTOR('',#6895,10.);
#1876=VECTOR('',#6904,10.);
#1877=VECTOR('',#6905,10.);
#1878=VECTOR('',#6906,10.);
#1879=VECTOR('',#6911,3.);
#1880=VECTOR('',#6918,3.);
#1881=VECTOR('',#6925,3.);
#1882=VECTOR('',#6932,3.);
#1883=VECTOR('',#6937,10.);
#1884=VECTOR('',#6938,10.);
#1885=VECTOR('',#6941,10.);
#1886=VECTOR('',#6944,10.);
#1887=VECTOR('',#6947,10.);
#1888=VECTOR('',#6950,10.);
#1889=VECTOR('',#6953,10.);
#1890=VECTOR('',#6954,10.);
#1891=VECTOR('',#6955,10.);
#1892=VECTOR('',#6956,10.);
#1893=VECTOR('',#6959,10.);
#1894=VECTOR('',#6960,10.);
#1895=VECTOR('',#6961,10.);
#1896=VECTOR('',#6962,10.);
#1897=VECTOR('',#6963,10.);
#1898=VECTOR('',#6964,10.);
#1899=VECTOR('',#6965,10.);
#1900=VECTOR('',#6966,10.);
#1901=VECTOR('',#6971,10.);
#1902=VECTOR('',#6974,10.);
#1903=VECTOR('',#6979,10.);
#1904=VECTOR('',#6982,10.);
#1905=VECTOR('',#6987,10.);
#1906=VECTOR('',#6990,10.);
#1907=VECTOR('',#6995,10.);
#1908=VECTOR('',#6998,10.);
#1909=VECTOR('',#7001,10.);
#1910=VECTOR('',#7004,10.);
#1911=VECTOR('',#7009,10.);
#1912=VECTOR('',#7012,10.);
#1913=VECTOR('',#7015,10.);
#1914=VECTOR('',#7016,10.);
#1915=VECTOR('',#7019,10.);
#1916=VECTOR('',#7020,10.);
#1917=VECTOR('',#7025,10.);
#1918=VECTOR('',#7026,10.);
#1919=VECTOR('',#7031,10.);
#1920=VECTOR('',#7032,10.);
#1921=VECTOR('',#7035,10.);
#1922=VECTOR('',#7036,10.);
#1923=VECTOR('',#7041,10.);
#1924=VECTOR('',#7042,10.);
#1925=VECTOR('',#7047,10.);
#1926=VECTOR('',#7048,10.);
#1927=VECTOR('',#7051,10.);
#1928=VECTOR('',#7052,10.);
#1929=VECTOR('',#7053,10.);
#1930=VECTOR('',#7056,10.);
#1931=VECTOR('',#7057,10.);
#1932=VECTOR('',#7060,10.);
#1933=VECTOR('',#7061,10.);
#1934=VECTOR('',#7064,10.);
#1935=VECTOR('',#7065,10.);
#1936=VECTOR('',#7068,10.);
#1937=VECTOR('',#7069,10.);
#1938=VECTOR('',#7072,10.);
#1939=VECTOR('',#7073,10.);
#1940=VECTOR('',#7080,10.);
#1941=VECTOR('',#7085,10.);
#1942=VECTOR('',#7088,10.);
#1943=VECTOR('',#7093,10.);
#1944=VECTOR('',#7118,10.);
#1945=VECTOR('',#7121,10.);
#1946=VECTOR('',#7124,10.);
#1947=VECTOR('',#7127,10.);
#1948=VECTOR('',#7130,10.);
#2360=CIRCLE('',#6076,4.);
#2361=CIRCLE('',#6077,1.);
#2362=CIRCLE('',#6078,5.);
#2363=CIRCLE('',#6080,4.);
#2364=CIRCLE('',#6082,1.);
#2365=CIRCLE('',#6083,5.);
#2366=CIRCLE('',#6086,4.);
#2367=CIRCLE('',#6087,1.);
#2368=CIRCLE('',#6088,5.);
#2369=CIRCLE('',#6090,4.);
#2370=CIRCLE('',#6092,1.);
#2371=CIRCLE('',#6093,5.);
#2372=CIRCLE('',#6096,3.);
#2373=CIRCLE('',#6097,3.);
#2374=CIRCLE('',#6099,3.);
#2375=CIRCLE('',#6100,3.);
#2376=CIRCLE('',#6102,3.);
#2377=CIRCLE('',#6103,3.);
#2378=CIRCLE('',#6105,3.);
#2379=CIRCLE('',#6106,3.);
#2500=VERTEX_POINT('',#8647);
#2501=VERTEX_POINT('',#8648);
#2502=VERTEX_POINT('',#8650);
#2503=VERTEX_POINT('',#8652);
#2504=VERTEX_POINT('',#8665);
#2505=VERTEX_POINT('',#8666);
#2506=VERTEX_POINT('',#8671);
#2507=VERTEX_POINT('',#8672);
#2508=VERTEX_POINT('',#8686);
#2509=VERTEX_POINT('',#8688);
#2510=VERTEX_POINT('',#8692);
#2511=VERTEX_POINT('',#8693);
#2512=VERTEX_POINT('',#8695);
#2513=VERTEX_POINT('',#8697);
#2514=VERTEX_POINT('',#8710);
#2515=VERTEX_POINT('',#8711);
#2516=VERTEX_POINT('',#8716);
#2517=VERTEX_POINT('',#8717);
#2518=VERTEX_POINT('',#8731);
#2519=VERTEX_POINT('',#8733);
#2520=VERTEX_POINT('',#8737);
#2521=VERTEX_POINT('',#8739);
#2522=VERTEX_POINT('',#8743);
#2523=VERTEX_POINT('',#8745);
#2524=VERTEX_POINT('',#8749);
#2525=VERTEX_POINT('',#8751);
#2526=VERTEX_POINT('',#8755);
#2527=VERTEX_POINT('',#8757);
#2528=VERTEX_POINT('',#8764);
#2529=VERTEX_POINT('',#8766);
#2530=VERTEX_POINT('',#8770);
#2531=VERTEX_POINT('',#8772);
#2532=VERTEX_POINT('',#8776);
#2533=VERTEX_POINT('',#8778);
#2534=VERTEX_POINT('',#8780);
#2535=VERTEX_POINT('',#8784);
#2536=VERTEX_POINT('',#8786);
#2537=VERTEX_POINT('',#8788);
#2538=VERTEX_POINT('',#8790);
#2539=VERTEX_POINT('',#8792);
#2540=VERTEX_POINT('',#8794);
#2541=VERTEX_POINT('',#8796);
#2542=VERTEX_POINT('',#8800);
#2543=VERTEX_POINT('',#8804);
#2544=VERTEX_POINT('',#8808);
#2545=VERTEX_POINT('',#8809);
#2546=VERTEX_POINT('',#8811);
#2547=VERTEX_POINT('',#8813);
#2548=VERTEX_POINT('',#8817);
#2549=VERTEX_POINT('',#8818);
#2550=VERTEX_POINT('',#8820);
#2551=VERTEX_POINT('',#8822);
#2552=VERTEX_POINT('',#8826);
#2553=VERTEX_POINT('',#8828);
#2554=VERTEX_POINT('',#8832);
#2555=VERTEX_POINT('',#8833);
#2556=VERTEX_POINT('',#8835);
#2557=VERTEX_POINT('',#8837);
#2558=VERTEX_POINT('',#8841);
#2559=VERTEX_POINT('',#8843);
#2560=VERTEX_POINT('',#8850);
#2561=VERTEX_POINT('',#8852);
#2562=VERTEX_POINT('',#8856);
#2563=VERTEX_POINT('',#8858);
#2564=VERTEX_POINT('',#8865);
#2565=VERTEX_POINT('',#8867);
#2566=VERTEX_POINT('',#8871);
#2567=VERTEX_POINT('',#8873);
#2568=VERTEX_POINT('',#8880);
#2569=VERTEX_POINT('',#8885);
#2570=VERTEX_POINT('',#8889);
#2571=VERTEX_POINT('',#8893);
#2572=VERTEX_POINT('',#8897);
#2573=VERTEX_POINT('',#8901);
#2574=VERTEX_POINT('',#8906);
#2575=VERTEX_POINT('',#8910);
#3021=EDGE_CURVE('',#2500,#2501,#2360,.T.);
#3022=EDGE_CURVE('',#2501,#2502,#2361,.T.);
#3023=EDGE_CURVE('',#2502,#2503,#207,.T.);
#3024=EDGE_CURVE('',#2503,#2500,#2362,.T.);
#3025=EDGE_CURVE('',#2504,#2505,#2363,.T.);
#3026=EDGE_CURVE('',#2505,#2501,#1319,.T.);
#3027=EDGE_CURVE('',#2500,#2504,#1320,.T.);
#3028=EDGE_CURVE('',#2506,#2507,#208,.T.);
#3029=EDGE_CURVE('',#2507,#2505,#2364,.T.);
#3030=EDGE_CURVE('',#2504,#2506,#2365,.T.);
#3031=EDGE_CURVE('',#2503,#2508,#1321,.T.);
#3032=EDGE_CURVE('',#2508,#2509,#1322,.T.);
#3033=EDGE_CURVE('',#2509,#2506,#1323,.T.);
#3034=EDGE_CURVE('',#2510,#2511,#2366,.T.);
#3035=EDGE_CURVE('',#2511,#2512,#2367,.T.);
#3036=EDGE_CURVE('',#2512,#2513,#209,.T.);
#3037=EDGE_CURVE('',#2513,#2510,#2368,.T.);
#3038=EDGE_CURVE('',#2514,#2515,#2369,.T.);
#3039=EDGE_CURVE('',#2515,#2511,#1324,.T.);
#3040=EDGE_CURVE('',#2510,#2514,#1325,.T.);
#3041=EDGE_CURVE('',#2516,#2517,#210,.T.);
#3042=EDGE_CURVE('',#2517,#2515,#2370,.T.);
#3043=EDGE_CURVE('',#2514,#2516,#2371,.T.);
#3044=EDGE_CURVE('',#2513,#2518,#1326,.T.);
#3045=EDGE_CURVE('',#2518,#2519,#1327,.T.);
#3046=EDGE_CURVE('',#2519,#2516,#1328,.T.);
#3047=EDGE_CURVE('',#2520,#2520,#2372,.T.);
#3048=EDGE_CURVE('',#2520,#2521,#1329,.T.);
#3049=EDGE_CURVE('',#2521,#2521,#2373,.T.);
#3050=EDGE_CURVE('',#2522,#2522,#2374,.T.);
#3051=EDGE_CURVE('',#2522,#2523,#1330,.T.);
#3052=EDGE_CURVE('',#2523,#2523,#2375,.T.);
#3053=EDGE_CURVE('',#2524,#2524,#2376,.T.);
#3054=EDGE_CURVE('',#2524,#2525,#1331,.T.);
#3055=EDGE_CURVE('',#2525,#2525,#2377,.T.);
#3056=EDGE_CURVE('',#2526,#2526,#2378,.T.);
#3057=EDGE_CURVE('',#2526,#2527,#1332,.T.);
#3058=EDGE_CURVE('',#2527,#2527,#2379,.T.);
#3059=EDGE_CURVE('',#2508,#2519,#1333,.T.);
#3060=EDGE_CURVE('',#2509,#2518,#1334,.T.);
#3061=EDGE_CURVE('',#2507,#2528,#1335,.T.);
#3062=EDGE_CURVE('',#2529,#2528,#51,.T.);
#3063=EDGE_CURVE('',#2529,#2505,#1336,.T.);
#3064=EDGE_CURVE('',#2511,#2530,#1337,.T.);
#3065=EDGE_CURVE('',#2530,#2531,#52,.T.);
#3066=EDGE_CURVE('',#2531,#2512,#1338,.T.);
#3067=EDGE_CURVE('',#2532,#2529,#1339,.T.);
#3068=EDGE_CURVE('',#2533,#2532,#1340,.T.);
#3069=EDGE_CURVE('',#2534,#2533,#1341,.T.);
#3070=EDGE_CURVE('',#2501,#2534,#1342,.T.);
#3071=EDGE_CURVE('',#2535,#2515,#1343,.T.);
#3072=EDGE_CURVE('',#2536,#2535,#1344,.T.);
#3073=EDGE_CURVE('',#2537,#2536,#1345,.T.);
#3074=EDGE_CURVE('',#2538,#2537,#1346,.T.);
#3075=EDGE_CURVE('',#2539,#2538,#1347,.T.);
#3076=EDGE_CURVE('',#2540,#2539,#1348,.T.);
#3077=EDGE_CURVE('',#2541,#2540,#1349,.T.);
#3078=EDGE_CURVE('',#2530,#2541,#1350,.T.);
#3079=EDGE_CURVE('',#2534,#2542,#53,.T.);
#3080=EDGE_CURVE('',#2542,#2502,#1351,.T.);
#3081=EDGE_CURVE('',#2517,#2543,#1352,.T.);
#3082=EDGE_CURVE('',#2535,#2543,#54,.T.);
#3083=EDGE_CURVE('',#2544,#2545,#1353,.T.);
#3084=EDGE_CURVE('',#2545,#2546,#55,.T.);
#3085=EDGE_CURVE('',#2546,#2547,#1354,.T.);
#3086=EDGE_CURVE('',#2544,#2547,#56,.T.);
#3087=EDGE_CURVE('',#2548,#2549,#1355,.T.);
#3088=EDGE_CURVE('',#2549,#2550,#57,.T.);
#3089=EDGE_CURVE('',#2550,#2551,#1356,.T.);
#3090=EDGE_CURVE('',#2551,#2548,#58,.T.);
#3091=EDGE_CURVE('',#2549,#2552,#1357,.T.);
#3092=EDGE_CURVE('',#2552,#2553,#59,.T.);
#3093=EDGE_CURVE('',#2553,#2550,#1358,.T.);
#3094=EDGE_CURVE('',#2554,#2555,#1359,.T.);
#3095=EDGE_CURVE('',#2555,#2556,#60,.T.);
#3096=EDGE_CURVE('',#2556,#2557,#1360,.T.);
#3097=EDGE_CURVE('',#2557,#2554,#61,.T.);
#3098=EDGE_CURVE('',#2552,#2558,#1361,.T.);
#3099=EDGE_CURVE('',#2558,#2559,#62,.T.);
#3100=EDGE_CURVE('',#2559,#2553,#1362,.T.);
#3101=EDGE_CURVE('',#2555,#2559,#1363,.T.);
#3102=EDGE_CURVE('',#2558,#2556,#1364,.T.);
#3103=EDGE_CURVE('',#2560,#2554,#1365,.T.);
#3104=EDGE_CURVE('',#2557,#2561,#1366,.T.);
#3105=EDGE_CURVE('',#2561,#2560,#63,.T.);
#3106=EDGE_CURVE('',#2562,#2560,#1367,.T.);
#3107=EDGE_CURVE('',#2561,#2563,#1368,.T.);
#3108=EDGE_CURVE('',#2563,#2562,#64,.T.);
#3109=EDGE_CURVE('',#2545,#2548,#1369,.T.);
#3110=EDGE_CURVE('',#2551,#2546,#1370,.T.);
#3111=EDGE_CURVE('',#2564,#2562,#1371,.T.);
#3112=EDGE_CURVE('',#2563,#2565,#1372,.T.);
#3113=EDGE_CURVE('',#2565,#2564,#65,.T.);
#3114=EDGE_CURVE('',#2566,#2564,#1373,.T.);
#3115=EDGE_CURVE('',#2565,#2567,#1374,.T.);
#3116=EDGE_CURVE('',#2567,#2566,#66,.T.);
#3117=EDGE_CURVE('',#2547,#2566,#1375,.T.);
#3118=EDGE_CURVE('',#2567,#2544,#1376,.T.);
#3119=EDGE_CURVE('',#2551,#2568,#1377,.T.);
#3120=EDGE_CURVE('',#2543,#2568,#1378,.T.);
#3121=EDGE_CURVE('',#2543,#2546,#1379,.T.);
#3122=EDGE_CURVE('',#2550,#2569,#1380,.T.);
#3123=EDGE_CURVE('',#2568,#2569,#1381,.T.);
#3124=EDGE_CURVE('',#2553,#2570,#1382,.T.);
#3125=EDGE_CURVE('',#2569,#2570,#1383,.T.);
#3126=EDGE_CURVE('',#2571,#2559,#1384,.T.);
#3127=EDGE_CURVE('',#2570,#2571,#1385,.T.);
#3128=EDGE_CURVE('',#2555,#2572,#1386,.T.);
#3129=EDGE_CURVE('',#2571,#2572,#1387,.T.);
#3130=EDGE_CURVE('',#2554,#2573,#1388,.T.);
#3131=EDGE_CURVE('',#2572,#2573,#1389,.T.);
#3132=EDGE_CURVE('',#2533,#2574,#67,.T.);
#3133=EDGE_CURVE('',#2574,#2542,#1390,.T.);
#3134=EDGE_CURVE('',#2532,#2575,#68,.T.);
#3135=EDGE_CURVE('',#2575,#2574,#1391,.T.);
#3136=EDGE_CURVE('',#2528,#2575,#1392,.T.);
#3137=EDGE_CURVE('',#2541,#2573,#69,.T.);
#3138=EDGE_CURVE('',#2573,#2531,#1393,.T.);
#3139=EDGE_CURVE('',#2540,#2572,#70,.T.);
#3140=EDGE_CURVE('',#2539,#2571,#71,.T.);
#3141=EDGE_CURVE('',#2538,#2570,#72,.T.);
#3142=EDGE_CURVE('',#2537,#2569,#73,.T.);
#3143=EDGE_CURVE('',#2536,#2568,#74,.T.);
#3144=EDGE_CURVE('',#2547,#2542,#1394,.T.);
#3145=EDGE_CURVE('',#2566,#2574,#1395,.T.);
#3146=EDGE_CURVE('',#2564,#2575,#1396,.T.);
#3147=EDGE_CURVE('',#2562,#2528,#1397,.T.);
#3148=EDGE_CURVE('',#2560,#2531,#1398,.T.);
#3938=ORIENTED_EDGE('',*,*,#3021,.T.);
#3939=ORIENTED_EDGE('',*,*,#3022,.T.);
#3940=ORIENTED_EDGE('',*,*,#3023,.T.);
#3941=ORIENTED_EDGE('',*,*,#3024,.T.);
#3942=ORIENTED_EDGE('',*,*,#3025,.T.);
#3943=ORIENTED_EDGE('',*,*,#3026,.T.);
#3944=ORIENTED_EDGE('',*,*,#3021,.F.);
#3945=ORIENTED_EDGE('',*,*,#3027,.T.);
#3946=ORIENTED_EDGE('',*,*,#3028,.T.);
#3947=ORIENTED_EDGE('',*,*,#3029,.T.);
#3948=ORIENTED_EDGE('',*,*,#3025,.F.);
#3949=ORIENTED_EDGE('',*,*,#3030,.T.);
#3950=ORIENTED_EDGE('',*,*,#3030,.F.);
#3951=ORIENTED_EDGE('',*,*,#3027,.F.);
#3952=ORIENTED_EDGE('',*,*,#3024,.F.);
#3953=ORIENTED_EDGE('',*,*,#3031,.T.);
#3954=ORIENTED_EDGE('',*,*,#3032,.T.);
#3955=ORIENTED_EDGE('',*,*,#3033,.T.);
#3956=ORIENTED_EDGE('',*,*,#3034,.T.);
#3957=ORIENTED_EDGE('',*,*,#3035,.T.);
#3958=ORIENTED_EDGE('',*,*,#3036,.T.);
#3959=ORIENTED_EDGE('',*,*,#3037,.T.);
#3960=ORIENTED_EDGE('',*,*,#3038,.T.);
#3961=ORIENTED_EDGE('',*,*,#3039,.T.);
#3962=ORIENTED_EDGE('',*,*,#3034,.F.);
#3963=ORIENTED_EDGE('',*,*,#3040,.T.);
#3964=ORIENTED_EDGE('',*,*,#3041,.T.);
#3965=ORIENTED_EDGE('',*,*,#3042,.T.);
#3966=ORIENTED_EDGE('',*,*,#3038,.F.);
#3967=ORIENTED_EDGE('',*,*,#3043,.T.);
#3968=ORIENTED_EDGE('',*,*,#3043,.F.);
#3969=ORIENTED_EDGE('',*,*,#3040,.F.);
#3970=ORIENTED_EDGE('',*,*,#3037,.F.);
#3971=ORIENTED_EDGE('',*,*,#3044,.T.);
#3972=ORIENTED_EDGE('',*,*,#3045,.T.);
#3973=ORIENTED_EDGE('',*,*,#3046,.T.);
#3974=ORIENTED_EDGE('',*,*,#3047,.F.);
#3975=ORIENTED_EDGE('',*,*,#3048,.T.);
#3976=ORIENTED_EDGE('',*,*,#3049,.F.);
#3977=ORIENTED_EDGE('',*,*,#3048,.F.);
#3978=ORIENTED_EDGE('',*,*,#3050,.F.);
#3979=ORIENTED_EDGE('',*,*,#3051,.T.);
#3980=ORIENTED_EDGE('',*,*,#3052,.F.);
#3981=ORIENTED_EDGE('',*,*,#3051,.F.);
#3982=ORIENTED_EDGE('',*,*,#3053,.F.);
#3983=ORIENTED_EDGE('',*,*,#3054,.T.);
#3984=ORIENTED_EDGE('',*,*,#3055,.F.);
#3985=ORIENTED_EDGE('',*,*,#3054,.F.);
#3986=ORIENTED_EDGE('',*,*,#3056,.F.);
#3987=ORIENTED_EDGE('',*,*,#3057,.T.);
#3988=ORIENTED_EDGE('',*,*,#3058,.F.);
#3989=ORIENTED_EDGE('',*,*,#3057,.F.);
#3990=ORIENTED_EDGE('',*,*,#3059,.T.);
#3991=ORIENTED_EDGE('',*,*,#3045,.F.);
#3992=ORIENTED_EDGE('',*,*,#3060,.F.);
#3993=ORIENTED_EDGE('',*,*,#3032,.F.);
#3994=ORIENTED_EDGE('',*,*,#3029,.F.);
#3995=ORIENTED_EDGE('',*,*,#3061,.T.);
#3996=ORIENTED_EDGE('',*,*,#3062,.F.);
#3997=ORIENTED_EDGE('',*,*,#3063,.T.);
#3998=ORIENTED_EDGE('',*,*,#3035,.F.);
#3999=ORIENTED_EDGE('',*,*,#3064,.T.);
#4000=ORIENTED_EDGE('',*,*,#3065,.T.);
#4001=ORIENTED_EDGE('',*,*,#3066,.T.);
#4002=ORIENTED_EDGE('',*,*,#3026,.F.);
#4003=ORIENTED_EDGE('',*,*,#3063,.F.);
#4004=ORIENTED_EDGE('',*,*,#3067,.F.);
#4005=ORIENTED_EDGE('',*,*,#3068,.F.);
#4006=ORIENTED_EDGE('',*,*,#3069,.F.);
#4007=ORIENTED_EDGE('',*,*,#3070,.F.);
#4008=ORIENTED_EDGE('',*,*,#3047,.T.);
#4009=ORIENTED_EDGE('',*,*,#3053,.T.);
#4010=ORIENTED_EDGE('',*,*,#3039,.F.);
#4011=ORIENTED_EDGE('',*,*,#3071,.F.);
#4012=ORIENTED_EDGE('',*,*,#3072,.F.);
#4013=ORIENTED_EDGE('',*,*,#3073,.F.);
#4014=ORIENTED_EDGE('',*,*,#3074,.F.);
#4015=ORIENTED_EDGE('',*,*,#3075,.F.);
#4016=ORIENTED_EDGE('',*,*,#3076,.F.);
#4017=ORIENTED_EDGE('',*,*,#3077,.F.);
#4018=ORIENTED_EDGE('',*,*,#3078,.F.);
#4019=ORIENTED_EDGE('',*,*,#3064,.F.);
#4020=ORIENTED_EDGE('',*,*,#3050,.T.);
#4021=ORIENTED_EDGE('',*,*,#3056,.T.);
#4022=ORIENTED_EDGE('',*,*,#3022,.F.);
#4023=ORIENTED_EDGE('',*,*,#3070,.T.);
#4024=ORIENTED_EDGE('',*,*,#3079,.T.);
#4025=ORIENTED_EDGE('',*,*,#3080,.T.);
#4026=ORIENTED_EDGE('',*,*,#3042,.F.);
#4027=ORIENTED_EDGE('',*,*,#3081,.T.);
#4028=ORIENTED_EDGE('',*,*,#3082,.F.);
#4029=ORIENTED_EDGE('',*,*,#3071,.T.);
#4030=ORIENTED_EDGE('',*,*,#3083,.T.);
#4031=ORIENTED_EDGE('',*,*,#3084,.T.);
#4032=ORIENTED_EDGE('',*,*,#3085,.T.);
#4033=ORIENTED_EDGE('',*,*,#3086,.F.);
#4034=ORIENTED_EDGE('',*,*,#3087,.T.);
#4035=ORIENTED_EDGE('',*,*,#3088,.T.);
#4036=ORIENTED_EDGE('',*,*,#3089,.T.);
#4037=ORIENTED_EDGE('',*,*,#3090,.T.);
#4038=ORIENTED_EDGE('',*,*,#3091,.T.);
#4039=ORIENTED_EDGE('',*,*,#3092,.T.);
#4040=ORIENTED_EDGE('',*,*,#3093,.T.);
#4041=ORIENTED_EDGE('',*,*,#3088,.F.);
#4042=ORIENTED_EDGE('',*,*,#3094,.T.);
#4043=ORIENTED_EDGE('',*,*,#3095,.T.);
#4044=ORIENTED_EDGE('',*,*,#3096,.T.);
#4045=ORIENTED_EDGE('',*,*,#3097,.T.);
#4046=ORIENTED_EDGE('',*,*,#3098,.T.);
#4047=ORIENTED_EDGE('',*,*,#3099,.T.);
#4048=ORIENTED_EDGE('',*,*,#3100,.T.);
#4049=ORIENTED_EDGE('',*,*,#3092,.F.);
#4050=ORIENTED_EDGE('',*,*,#3101,.T.);
#4051=ORIENTED_EDGE('',*,*,#3099,.F.);
#4052=ORIENTED_EDGE('',*,*,#3102,.T.);
#4053=ORIENTED_EDGE('',*,*,#3095,.F.);
#4054=ORIENTED_EDGE('',*,*,#3103,.T.);
#4055=ORIENTED_EDGE('',*,*,#3097,.F.);
#4056=ORIENTED_EDGE('',*,*,#3104,.T.);
#4057=ORIENTED_EDGE('',*,*,#3105,.T.);
#4058=ORIENTED_EDGE('',*,*,#3106,.T.);
#4059=ORIENTED_EDGE('',*,*,#3105,.F.);
#4060=ORIENTED_EDGE('',*,*,#3107,.T.);
#4061=ORIENTED_EDGE('',*,*,#3108,.T.);
#4062=ORIENTED_EDGE('',*,*,#3109,.T.);
#4063=ORIENTED_EDGE('',*,*,#3090,.F.);
#4064=ORIENTED_EDGE('',*,*,#3110,.T.);
#4065=ORIENTED_EDGE('',*,*,#3084,.F.);
#4066=ORIENTED_EDGE('',*,*,#3111,.T.);
#4067=ORIENTED_EDGE('',*,*,#3108,.F.);
#4068=ORIENTED_EDGE('',*,*,#3112,.T.);
#4069=ORIENTED_EDGE('',*,*,#3113,.T.);
#4070=ORIENTED_EDGE('',*,*,#3114,.T.);
#4071=ORIENTED_EDGE('',*,*,#3113,.F.);
#4072=ORIENTED_EDGE('',*,*,#3115,.T.);
#4073=ORIENTED_EDGE('',*,*,#3116,.T.);
#4074=ORIENTED_EDGE('',*,*,#3117,.T.);
#4075=ORIENTED_EDGE('',*,*,#3116,.F.);
#4076=ORIENTED_EDGE('',*,*,#3118,.T.);
#4077=ORIENTED_EDGE('',*,*,#3086,.T.);
#4078=ORIENTED_EDGE('',*,*,#3110,.F.);
#4079=ORIENTED_EDGE('',*,*,#3119,.T.);
#4080=ORIENTED_EDGE('',*,*,#3120,.F.);
#4081=ORIENTED_EDGE('',*,*,#3121,.T.);
#4082=ORIENTED_EDGE('',*,*,#3089,.F.);
#4083=ORIENTED_EDGE('',*,*,#3122,.T.);
#4084=ORIENTED_EDGE('',*,*,#3123,.F.);
#4085=ORIENTED_EDGE('',*,*,#3119,.F.);
#4086=ORIENTED_EDGE('',*,*,#3093,.F.);
#4087=ORIENTED_EDGE('',*,*,#3124,.T.);
#4088=ORIENTED_EDGE('',*,*,#3125,.F.);
#4089=ORIENTED_EDGE('',*,*,#3122,.F.);
#4090=ORIENTED_EDGE('',*,*,#3100,.F.);
#4091=ORIENTED_EDGE('',*,*,#3126,.F.);
#4092=ORIENTED_EDGE('',*,*,#3127,.F.);
#4093=ORIENTED_EDGE('',*,*,#3124,.F.);
#4094=ORIENTED_EDGE('',*,*,#3101,.F.);
#4095=ORIENTED_EDGE('',*,*,#3128,.T.);
#4096=ORIENTED_EDGE('',*,*,#3129,.F.);
#4097=ORIENTED_EDGE('',*,*,#3126,.T.);
#4098=ORIENTED_EDGE('',*,*,#3094,.F.);
#4099=ORIENTED_EDGE('',*,*,#3130,.T.);
#4100=ORIENTED_EDGE('',*,*,#3131,.F.);
#4101=ORIENTED_EDGE('',*,*,#3128,.F.);
#4102=ORIENTED_EDGE('',*,*,#3096,.F.);
#4103=ORIENTED_EDGE('',*,*,#3102,.F.);
#4104=ORIENTED_EDGE('',*,*,#3098,.F.);
#4105=ORIENTED_EDGE('',*,*,#3091,.F.);
#4106=ORIENTED_EDGE('',*,*,#3087,.F.);
#4107=ORIENTED_EDGE('',*,*,#3109,.F.);
#4108=ORIENTED_EDGE('',*,*,#3083,.F.);
#4109=ORIENTED_EDGE('',*,*,#3118,.F.);
#4110=ORIENTED_EDGE('',*,*,#3115,.F.);
#4111=ORIENTED_EDGE('',*,*,#3112,.F.);
#4112=ORIENTED_EDGE('',*,*,#3107,.F.);
#4113=ORIENTED_EDGE('',*,*,#3104,.F.);
#4114=ORIENTED_EDGE('',*,*,#3049,.T.);
#4115=ORIENTED_EDGE('',*,*,#3052,.T.);
#4116=ORIENTED_EDGE('',*,*,#3055,.T.);
#4117=ORIENTED_EDGE('',*,*,#3058,.T.);
#4118=ORIENTED_EDGE('',*,*,#3069,.T.);
#4119=ORIENTED_EDGE('',*,*,#3132,.T.);
#4120=ORIENTED_EDGE('',*,*,#3133,.T.);
#4121=ORIENTED_EDGE('',*,*,#3079,.F.);
#4122=ORIENTED_EDGE('',*,*,#3068,.T.);
#4123=ORIENTED_EDGE('',*,*,#3134,.T.);
#4124=ORIENTED_EDGE('',*,*,#3135,.T.);
#4125=ORIENTED_EDGE('',*,*,#3132,.F.);
#4126=ORIENTED_EDGE('',*,*,#3067,.T.);
#4127=ORIENTED_EDGE('',*,*,#3062,.T.);
#4128=ORIENTED_EDGE('',*,*,#3136,.T.);
#4129=ORIENTED_EDGE('',*,*,#3134,.F.);
#4130=ORIENTED_EDGE('',*,*,#3078,.T.);
#4131=ORIENTED_EDGE('',*,*,#3137,.T.);
#4132=ORIENTED_EDGE('',*,*,#3138,.T.);
#4133=ORIENTED_EDGE('',*,*,#3065,.F.);
#4134=ORIENTED_EDGE('',*,*,#3077,.T.);
#4135=ORIENTED_EDGE('',*,*,#3139,.T.);
#4136=ORIENTED_EDGE('',*,*,#3131,.T.);
#4137=ORIENTED_EDGE('',*,*,#3137,.F.);
#4138=ORIENTED_EDGE('',*,*,#3129,.T.);
#4139=ORIENTED_EDGE('',*,*,#3139,.F.);
#4140=ORIENTED_EDGE('',*,*,#3076,.T.);
#4141=ORIENTED_EDGE('',*,*,#3140,.T.);
#4142=ORIENTED_EDGE('',*,*,#3127,.T.);
#4143=ORIENTED_EDGE('',*,*,#3140,.F.);
#4144=ORIENTED_EDGE('',*,*,#3075,.T.);
#4145=ORIENTED_EDGE('',*,*,#3141,.T.);
#4146=ORIENTED_EDGE('',*,*,#3125,.T.);
#4147=ORIENTED_EDGE('',*,*,#3141,.F.);
#4148=ORIENTED_EDGE('',*,*,#3074,.T.);
#4149=ORIENTED_EDGE('',*,*,#3142,.T.);
#4150=ORIENTED_EDGE('',*,*,#3123,.T.);
#4151=ORIENTED_EDGE('',*,*,#3142,.F.);
#4152=ORIENTED_EDGE('',*,*,#3073,.T.);
#4153=ORIENTED_EDGE('',*,*,#3143,.T.);
#4154=ORIENTED_EDGE('',*,*,#3120,.T.);
#4155=ORIENTED_EDGE('',*,*,#3143,.F.);
#4156=ORIENTED_EDGE('',*,*,#3072,.T.);
#4157=ORIENTED_EDGE('',*,*,#3082,.T.);
#4158=ORIENTED_EDGE('',*,*,#3085,.F.);
#4159=ORIENTED_EDGE('',*,*,#3121,.F.);
#4160=ORIENTED_EDGE('',*,*,#3081,.F.);
#4161=ORIENTED_EDGE('',*,*,#3041,.F.);
#4162=ORIENTED_EDGE('',*,*,#3046,.F.);
#4163=ORIENTED_EDGE('',*,*,#3059,.F.);
#4164=ORIENTED_EDGE('',*,*,#3031,.F.);
#4165=ORIENTED_EDGE('',*,*,#3023,.F.);
#4166=ORIENTED_EDGE('',*,*,#3080,.F.);
#4167=ORIENTED_EDGE('',*,*,#3144,.F.);
#4168=ORIENTED_EDGE('',*,*,#3117,.F.);
#4169=ORIENTED_EDGE('',*,*,#3144,.T.);
#4170=ORIENTED_EDGE('',*,*,#3133,.F.);
#4171=ORIENTED_EDGE('',*,*,#3145,.F.);
#4172=ORIENTED_EDGE('',*,*,#3114,.F.);
#4173=ORIENTED_EDGE('',*,*,#3145,.T.);
#4174=ORIENTED_EDGE('',*,*,#3135,.F.);
#4175=ORIENTED_EDGE('',*,*,#3146,.F.);
#4176=ORIENTED_EDGE('',*,*,#3111,.F.);
#4177=ORIENTED_EDGE('',*,*,#3146,.T.);
#4178=ORIENTED_EDGE('',*,*,#3136,.F.);
#4179=ORIENTED_EDGE('',*,*,#3147,.F.);
#4180=ORIENTED_EDGE('',*,*,#3106,.F.);
#4181=ORIENTED_EDGE('',*,*,#3147,.T.);
#4182=ORIENTED_EDGE('',*,*,#3061,.F.);
#4183=ORIENTED_EDGE('',*,*,#3028,.F.);
#4184=ORIENTED_EDGE('',*,*,#3033,.F.);
#4185=ORIENTED_EDGE('',*,*,#3060,.T.);
#4186=ORIENTED_EDGE('',*,*,#3044,.F.);
#4187=ORIENTED_EDGE('',*,*,#3036,.F.);
#4188=ORIENTED_EDGE('',*,*,#3066,.F.);
#4189=ORIENTED_EDGE('',*,*,#3148,.F.);
#4190=ORIENTED_EDGE('',*,*,#3103,.F.);
#4191=ORIENTED_EDGE('',*,*,#3148,.T.);
#4192=ORIENTED_EDGE('',*,*,#3138,.F.);
#4193=ORIENTED_EDGE('',*,*,#3130,.F.);
#5341=CYLINDRICAL_SURFACE('',#6079,4.);
#5342=CYLINDRICAL_SURFACE('',#6089,4.);
#5343=CYLINDRICAL_SURFACE('',#6095,3.);
#5344=CYLINDRICAL_SURFACE('',#6098,3.);
#5345=CYLINDRICAL_SURFACE('',#6101,3.);
#5346=CYLINDRICAL_SURFACE('',#6104,3.);
#5347=CYLINDRICAL_SURFACE('',#6108,1.);
#5348=CYLINDRICAL_SURFACE('',#6110,1.);
#5349=CYLINDRICAL_SURFACE('',#6114,1.);
#5350=CYLINDRICAL_SURFACE('',#6116,1.);
#5351=CYLINDRICAL_SURFACE('',#6118,1.);
#5352=CYLINDRICAL_SURFACE('',#6121,1.);
#5353=CYLINDRICAL_SURFACE('',#6124,1.);
#5354=CYLINDRICAL_SURFACE('',#6126,1.);
#5355=CYLINDRICAL_SURFACE('',#6129,1.);
#5356=CYLINDRICAL_SURFACE('',#6131,1.);
#5357=CYLINDRICAL_SURFACE('',#6132,1.);
#5358=CYLINDRICAL_SURFACE('',#6134,1.);
#5359=CYLINDRICAL_SURFACE('',#6136,1.);
#5360=CYLINDRICAL_SURFACE('',#6137,1.);
#5361=CYLINDRICAL_SURFACE('',#6139,1.);
#5362=CYLINDRICAL_SURFACE('',#6141,1.);
#5363=CYLINDRICAL_SURFACE('',#6149,1.);
#5364=CYLINDRICAL_SURFACE('',#6151,1.);
#5365=CYLINDRICAL_SURFACE('',#6153,1.);
#5366=CYLINDRICAL_SURFACE('',#6154,1.);
#5367=CYLINDRICAL_SURFACE('',#6156,1.);
#5368=CYLINDRICAL_SURFACE('',#6158,1.);
#5369=CYLINDRICAL_SURFACE('',#6160,1.);
#5370=CYLINDRICAL_SURFACE('',#6162,1.);
#5371=CYLINDRICAL_SURFACE('',#6164,1.);
#5372=CYLINDRICAL_SURFACE('',#6166,1.);
#5575=ADVANCED_FACE('',(#512),#211,.F.);
#5576=ADVANCED_FACE('',(#513),#5341,.F.);
#5577=ADVANCED_FACE('',(#514),#212,.F.);
#5578=ADVANCED_FACE('',(#515),#356,.T.);
#5579=ADVANCED_FACE('',(#516),#213,.F.);
#5580=ADVANCED_FACE('',(#517),#5342,.F.);
#5581=ADVANCED_FACE('',(#518),#214,.F.);
#5582=ADVANCED_FACE('',(#519),#357,.T.);
#5583=ADVANCED_FACE('',(#520),#5343,.F.);
#5584=ADVANCED_FACE('',(#521),#5344,.F.);
#5585=ADVANCED_FACE('',(#522),#5345,.F.);
#5586=ADVANCED_FACE('',(#523),#5346,.F.);
#5587=ADVANCED_FACE('',(#524),#358,.T.);
#5588=ADVANCED_FACE('',(#525),#5347,.T.);
#5589=ADVANCED_FACE('',(#526),#5348,.T.);
#5590=ADVANCED_FACE('',(#527,#273,#274),#359,.T.);
#5591=ADVANCED_FACE('',(#528,#275,#276),#360,.T.);
#5592=ADVANCED_FACE('',(#529),#5349,.T.);
#5593=ADVANCED_FACE('',(#530),#5350,.T.);
#5594=ADVANCED_FACE('',(#531),#5351,.T.);
#5595=ADVANCED_FACE('',(#532),#5352,.T.);
#5596=ADVANCED_FACE('',(#533),#5353,.T.);
#5597=ADVANCED_FACE('',(#534),#5354,.T.);
#5598=ADVANCED_FACE('',(#535),#5355,.T.);
#5599=ADVANCED_FACE('',(#536),#5356,.T.);
#5600=ADVANCED_FACE('',(#537),#5357,.T.);
#5601=ADVANCED_FACE('',(#538),#5358,.T.);
#5602=ADVANCED_FACE('',(#539),#5359,.T.);
#5603=ADVANCED_FACE('',(#540),#5360,.T.);
#5604=ADVANCED_FACE('',(#541),#5361,.T.);
#5605=ADVANCED_FACE('',(#542),#5362,.T.);
#5606=ADVANCED_FACE('',(#543),#361,.T.);
#5607=ADVANCED_FACE('',(#544),#362,.T.);
#5608=ADVANCED_FACE('',(#545),#363,.T.);
#5609=ADVANCED_FACE('',(#546),#364,.T.);
#5610=ADVANCED_FACE('',(#547),#365,.T.);
#5611=ADVANCED_FACE('',(#548),#366,.T.);
#5612=ADVANCED_FACE('',(#549,#277,#278,#279,#280),#367,.F.);
#5613=ADVANCED_FACE('',(#550),#5363,.T.);
#5614=ADVANCED_FACE('',(#551),#5364,.T.);
#5615=ADVANCED_FACE('',(#552),#5365,.T.);
#5616=ADVANCED_FACE('',(#553),#5366,.T.);
#5617=ADVANCED_FACE('',(#554),#5367,.T.);
#5618=ADVANCED_FACE('',(#555),#5368,.T.);
#5619=ADVANCED_FACE('',(#556),#5369,.T.);
#5620=ADVANCED_FACE('',(#557),#5370,.T.);
#5621=ADVANCED_FACE('',(#558),#5371,.T.);
#5622=ADVANCED_FACE('',(#559),#5372,.T.);
#5623=ADVANCED_FACE('',(#560),#368,.T.);
#5624=ADVANCED_FACE('',(#561),#369,.T.);
#5625=ADVANCED_FACE('',(#562),#370,.T.);
#5626=ADVANCED_FACE('',(#563),#371,.T.);
#5627=ADVANCED_FACE('',(#564),#372,.T.);
#5628=ADVANCED_FACE('',(#565),#373,.T.);
#5881=CLOSED_SHELL('',(#5575,#5576,#5577,#5578,#5579,#5580,#5581,#5582,
#5583,#5584,#5585,#5586,#5587,#5588,#5589,#5590,#5591,#5592,#5593,#5594,
#5595,#5596,#5597,#5598,#5599,#5600,#5601,#5602,#5603,#5604,#5605,#5606,
#5607,#5608,#5609,#5610,#5611,#5612,#5613,#5614,#5615,#5616,#5617,#5618,
#5619,#5620,#5621,#5622,#5623,#5624,#5625,#5626,#5627,#5628));
#6074=AXIS2_PLACEMENT_3D('',#8645,#6855,#6856);
#6075=AXIS2_PLACEMENT_3D('',#8646,#6857,#6858);
#6076=AXIS2_PLACEMENT_3D('',#8649,#6859,#6860);
#6077=AXIS2_PLACEMENT_3D('',#8651,#6861,#6862);
#6078=AXIS2_PLACEMENT_3D('',#8663,#6863,#6864);
#6079=AXIS2_PLACEMENT_3D('',#8664,#6865,#6866);
#6080=AXIS2_PLACEMENT_3D('',#8667,#6867,#6868);
#6081=AXIS2_PLACEMENT_3D('',#8670,#6871,#6872);
#6082=AXIS2_PLACEMENT_3D('',#8683,#6873,#6874);
#6083=AXIS2_PLACEMENT_3D('',#8684,#6875,#6876);
#6084=AXIS2_PLACEMENT_3D('',#8685,#6877,#6878);
#6085=AXIS2_PLACEMENT_3D('',#8691,#6882,#6883);
#6086=AXIS2_PLACEMENT_3D('',#8694,#6884,#6885);
#6087=AXIS2_PLACEMENT_3D('',#8696,#6886,#6887);
#6088=AXIS2_PLACEMENT_3D('',#8708,#6888,#6889);
#6089=AXIS2_PLACEMENT_3D('',#8709,#6890,#6891);
#6090=AXIS2_PLACEMENT_3D('',#8712,#6892,#6893);
#6091=AXIS2_PLACEMENT_3D('',#8715,#6896,#6897);
#6092=AXIS2_PLACEMENT_3D('',#8728,#6898,#6899);
#6093=AXIS2_PLACEMENT_3D('',#8729,#6900,#6901);
#6094=AXIS2_PLACEMENT_3D('',#8730,#6902,#6903);
#6095=AXIS2_PLACEMENT_3D('',#8736,#6907,#6908);
#6096=AXIS2_PLACEMENT_3D('',#8738,#6909,#6910);
#6097=AXIS2_PLACEMENT_3D('',#8741,#6912,#6913);
#6098=AXIS2_PLACEMENT_3D('',#8742,#6914,#6915);
#6099=AXIS2_PLACEMENT_3D('',#8744,#6916,#6917);
#6100=AXIS2_PLACEMENT_3D('',#8747,#6919,#6920);
#6101=AXIS2_PLACEMENT_3D('',#8748,#6921,#6922);
#6102=AXIS2_PLACEMENT_3D('',#8750,#6923,#6924);
#6103=AXIS2_PLACEMENT_3D('',#8753,#6926,#6927);
#6104=AXIS2_PLACEMENT_3D('',#8754,#6928,#6929);
#6105=AXIS2_PLACEMENT_3D('',#8756,#6930,#6931);
#6106=AXIS2_PLACEMENT_3D('',#8759,#6933,#6934);
#6107=AXIS2_PLACEMENT_3D('',#8760,#6935,#6936);
#6108=AXIS2_PLACEMENT_3D('',#8763,#6939,#6940);
#6109=AXIS2_PLACEMENT_3D('',#8767,#6942,#6943);
#6110=AXIS2_PLACEMENT_3D('',#8769,#6945,#6946);
#6111=AXIS2_PLACEMENT_3D('',#8773,#6948,#6949);
#6112=AXIS2_PLACEMENT_3D('',#8775,#6951,#6952);
#6113=AXIS2_PLACEMENT_3D('',#8783,#6957,#6958);
#6114=AXIS2_PLACEMENT_3D('',#8799,#6967,#6968);
#6115=AXIS2_PLACEMENT_3D('',#8801,#6969,#6970);
#6116=AXIS2_PLACEMENT_3D('',#8803,#6972,#6973);
#6117=AXIS2_PLACEMENT_3D('',#8806,#6975,#6976);
#6118=AXIS2_PLACEMENT_3D('',#8807,#6977,#6978);
#6119=AXIS2_PLACEMENT_3D('',#8812,#6980,#6981);
#6120=AXIS2_PLACEMENT_3D('',#8815,#6983,#6984);
#6121=AXIS2_PLACEMENT_3D('',#8816,#6985,#6986);
#6122=AXIS2_PLACEMENT_3D('',#8821,#6988,#6989);
#6123=AXIS2_PLACEMENT_3D('',#8824,#6991,#6992);
#6124=AXIS2_PLACEMENT_3D('',#8825,#6993,#6994);
#6125=AXIS2_PLACEMENT_3D('',#8829,#6996,#6997);
#6126=AXIS2_PLACEMENT_3D('',#8831,#6999,#7000);
#6127=AXIS2_PLACEMENT_3D('',#8836,#7002,#7003);
#6128=AXIS2_PLACEMENT_3D('',#8839,#7005,#7006);
#6129=AXIS2_PLACEMENT_3D('',#8840,#7007,#7008);
#6130=AXIS2_PLACEMENT_3D('',#8844,#7010,#7011);
#6131=AXIS2_PLACEMENT_3D('',#8846,#7013,#7014);
#6132=AXIS2_PLACEMENT_3D('',#8849,#7017,#7018);
#6133=AXIS2_PLACEMENT_3D('',#8854,#7021,#7022);
#6134=AXIS2_PLACEMENT_3D('',#8855,#7023,#7024);
#6135=AXIS2_PLACEMENT_3D('',#8860,#7027,#7028);
#6136=AXIS2_PLACEMENT_3D('',#8861,#7029,#7030);
#6137=AXIS2_PLACEMENT_3D('',#8864,#7033,#7034);
#6138=AXIS2_PLACEMENT_3D('',#8869,#7037,#7038);
#6139=AXIS2_PLACEMENT_3D('',#8870,#7039,#7040);
#6140=AXIS2_PLACEMENT_3D('',#8875,#7043,#7044);
#6141=AXIS2_PLACEMENT_3D('',#8876,#7045,#7046);
#6142=AXIS2_PLACEMENT_3D('',#8879,#7049,#7050);
#6143=AXIS2_PLACEMENT_3D('',#8884,#7054,#7055);
#6144=AXIS2_PLACEMENT_3D('',#8888,#7058,#7059);
#6145=AXIS2_PLACEMENT_3D('',#8892,#7062,#7063);
#6146=AXIS2_PLACEMENT_3D('',#8896,#7066,#7067);
#6147=AXIS2_PLACEMENT_3D('',#8900,#7070,#7071);
#6148=AXIS2_PLACEMENT_3D('',#8904,#7074,#7075);
#6149=AXIS2_PLACEMENT_3D('',#8905,#7076,#7077);
#6150=AXIS2_PLACEMENT_3D('',#8907,#7078,#7079);
#6151=AXIS2_PLACEMENT_3D('',#8909,#7081,#7082);
#6152=AXIS2_PLACEMENT_3D('',#8911,#7083,#7084);
#6153=AXIS2_PLACEMENT_3D('',#8913,#7086,#7087);
#6154=AXIS2_PLACEMENT_3D('',#8915,#7089,#7090);
#6155=AXIS2_PLACEMENT_3D('',#8916,#7091,#7092);
#6156=AXIS2_PLACEMENT_3D('',#8918,#7094,#7095);
#6157=AXIS2_PLACEMENT_3D('',#8919,#7096,#7097);
#6158=AXIS2_PLACEMENT_3D('',#8920,#7098,#7099);
#6159=AXIS2_PLACEMENT_3D('',#8921,#7100,#7101);
#6160=AXIS2_PLACEMENT_3D('',#8922,#7102,#7103);
#6161=AXIS2_PLACEMENT_3D('',#8923,#7104,#7105);
#6162=AXIS2_PLACEMENT_3D('',#8924,#7106,#7107);
#6163=AXIS2_PLACEMENT_3D('',#8925,#7108,#7109);
#6164=AXIS2_PLACEMENT_3D('',#8926,#7110,#7111);
#6165=AXIS2_PLACEMENT_3D('',#8927,#7112,#7113);
#6166=AXIS2_PLACEMENT_3D('',#8928,#7114,#7115);
#6167=AXIS2_PLACEMENT_3D('',#8929,#7116,#7117);
#6168=AXIS2_PLACEMENT_3D('',#8931,#7119,#7120);
#6169=AXIS2_PLACEMENT_3D('',#8933,#7122,#7123);
#6170=AXIS2_PLACEMENT_3D('',#8935,#7125,#7126);
#6171=AXIS2_PLACEMENT_3D('',#8937,#7128,#7129);
#6172=AXIS2_PLACEMENT_3D('',#8939,#7131,#7132);
#6855=DIRECTION('axis',(0.,0.,1.));
#6856=DIRECTION('refdir',(1.,0.,0.));
#6857=DIRECTION('center_axis',(-1.,0.,0.));
#6858=DIRECTION('ref_axis',(0.,0.,1.));
#6859=DIRECTION('center_axis',(0.,1.,0.));
#6860=DIRECTION('ref_axis',(1.,0.,0.));
#6861=DIRECTION('center_axis',(1.,0.,0.));
#6862=DIRECTION('ref_axis',(0.,-0.707106781186552,0.707106781186543));
#6863=DIRECTION('center_axis',(-1.,0.,0.));
#6864=DIRECTION('ref_axis',(0.,-0.707106781186552,0.707106781186543));
#6865=DIRECTION('center_axis',(0.,1.,0.));
#6866=DIRECTION('ref_axis',(0.707106781186546,0.,-0.707106781186549));
#6867=DIRECTION('center_axis',(0.,1.,0.));
#6868=DIRECTION('ref_axis',(1.,0.,0.));
#6869=DIRECTION('',(0.,-1.,0.));
#6870=DIRECTION('',(0.,1.,0.));
#6871=DIRECTION('center_axis',(-1.,0.,0.));
#6872=DIRECTION('ref_axis',(0.,0.,1.));
#6873=DIRECTION('center_axis',(1.,0.,0.));
#6874=DIRECTION('ref_axis',(0.,0.707106781186548,0.707106781186548));
#6875=DIRECTION('center_axis',(-1.,0.,0.));
#6876=DIRECTION('ref_axis',(0.,0.707106781186547,0.707106781186547));
#6877=DIRECTION('center_axis',(-1.,0.,0.));
#6878=DIRECTION('ref_axis',(0.,0.,1.));
#6879=DIRECTION('',(0.,0.,1.));
#6880=DIRECTION('',(0.,0.965925826289068,-0.258819045102522));
#6881=DIRECTION('',(0.,0.,-1.));
#6882=DIRECTION('center_axis',(1.,0.,0.));
#6883=DIRECTION('ref_axis',(0.,0.,-1.));
#6884=DIRECTION('center_axis',(0.,-1.,0.));
#6885=DIRECTION('ref_axis',(-1.,0.,0.));
#6886=DIRECTION('center_axis',(-1.,0.,0.));
#6887=DIRECTION('ref_axis',(0.,0.707106781186548,0.707106781186548));
#6888=DIRECTION('center_axis',(1.,0.,0.));
#6889=DIRECTION('ref_axis',(0.,0.707106781186547,0.707106781186547));
#6890=DIRECTION('center_axis',(0.,-1.,0.));
#6891=DIRECTION('ref_axis',(-0.707106781186546,0.,-0.707106781186549));
#6892=DIRECTION('center_axis',(0.,-1.,0.));
#6893=DIRECTION('ref_axis',(-1.,0.,0.));
#6894=DIRECTION('',(0.,1.,0.));
#6895=DIRECTION('',(0.,-1.,0.));
#6896=DIRECTION('center_axis',(1.,0.,0.));
#6897=DIRECTION('ref_axis',(0.,0.,-1.));
#6898=DIRECTION('center_axis',(-1.,0.,0.));
#6899=DIRECTION('ref_axis',(0.,-0.707106781186552,0.707106781186543));
#6900=DIRECTION('center_axis',(1.,0.,0.));
#6901=DIRECTION('ref_axis',(0.,-0.707106781186552,0.707106781186543));
#6902=DIRECTION('center_axis',(1.,0.,0.));
#6903=DIRECTION('ref_axis',(0.,0.,-1.));
#6904=DIRECTION('',(0.,0.,1.));
#6905=DIRECTION('',(0.,-0.965925826289068,0.258819045102522));
#6906=DIRECTION('',(0.,0.,-1.));
#6907=DIRECTION('center_axis',(0.,0.,-1.));
#6908=DIRECTION('ref_axis',(-1.,0.,0.));
#6909=DIRECTION('center_axis',(0.,0.,-1.));
#6910=DIRECTION('ref_axis',(-1.,0.,0.));
#6911=DIRECTION('',(0.,0.,-1.));
#6912=DIRECTION('center_axis',(0.,0.,1.));
#6913=DIRECTION('ref_axis',(-1.,0.,0.));
#6914=DIRECTION('center_axis',(0.,0.,-1.));
#6915=DIRECTION('ref_axis',(-1.,0.,0.));
#6916=DIRECTION('center_axis',(0.,0.,-1.));
#6917=DIRECTION('ref_axis',(-1.,0.,0.));
#6918=DIRECTION('',(0.,0.,-1.));
#6919=DIRECTION('center_axis',(0.,0.,1.));
#6920=DIRECTION('ref_axis',(-1.,0.,0.));
#6921=DIRECTION('center_axis',(0.,0.,-1.));
#6922=DIRECTION('ref_axis',(-1.,0.,0.));
#6923=DIRECTION('center_axis',(0.,0.,-1.));
#6924=DIRECTION('ref_axis',(-1.,0.,0.));
#6925=DIRECTION('',(0.,0.,-1.));
#6926=DIRECTION('center_axis',(0.,0.,1.));
#6927=DIRECTION('ref_axis',(-1.,0.,0.));
#6928=DIRECTION('center_axis',(0.,0.,-1.));
#6929=DIRECTION('ref_axis',(-1.,0.,0.));
#6930=DIRECTION('center_axis',(0.,0.,-1.));
#6931=DIRECTION('ref_axis',(-1.,0.,0.));
#6932=DIRECTION('',(0.,0.,-1.));
#6933=DIRECTION('center_axis',(0.,0.,1.));
#6934=DIRECTION('ref_axis',(-1.,0.,0.));
#6935=DIRECTION('center_axis',(0.,0.258819045102522,0.965925826289068));
#6936=DIRECTION('ref_axis',(0.,-0.965925826289068,0.258819045102522));
#6937=DIRECTION('',(1.,0.,0.));
#6938=DIRECTION('',(1.,0.,0.));
#6939=DIRECTION('center_axis',(-1.,0.,0.));
#6940=DIRECTION('ref_axis',(0.,0.707106781186554,0.707106781186541));
#6941=DIRECTION('',(-1.,0.,0.));
#6942=DIRECTION('center_axis',(-0.923879532511286,-0.382683432365092,0.));
#6943=DIRECTION('ref_axis',(-0.382683432365092,0.923879532511286,0.));
#6944=DIRECTION('',(1.,0.,0.));
#6945=DIRECTION('center_axis',(-1.,0.,0.));
#6946=DIRECTION('ref_axis',(0.,0.707106781186554,0.707106781186541));
#6947=DIRECTION('',(1.,0.,0.));
#6948=DIRECTION('center_axis',(-0.923879532511286,0.382683432365092,0.));
#6949=DIRECTION('ref_axis',(0.382683432365092,0.923879532511286,0.));
#6950=DIRECTION('',(-1.,0.,0.));
#6951=DIRECTION('center_axis',(0.,0.,1.));
#6952=DIRECTION('ref_axis',(1.,0.,0.));
#6953=DIRECTION('',(0.707106781186548,0.707106781186548,0.));
#6954=DIRECTION('',(0.,1.,0.));
#6955=DIRECTION('',(-0.707106781186548,0.707106781186548,0.));
#6956=DIRECTION('',(-1.,0.,0.));
#6957=DIRECTION('center_axis',(0.,0.,1.));
#6958=DIRECTION('ref_axis',(1.,0.,0.));
#6959=DIRECTION('',(-1.,0.,0.));
#6960=DIRECTION('',(-0.707106781186548,-0.707106781186548,0.));
#6961=DIRECTION('',(0.,-1.,0.));
#6962=DIRECTION('',(-0.707106781186548,-0.707106781186548,0.));
#6963=DIRECTION('',(-1.,-4.56509835347174E-16,0.));
#6964=DIRECTION('',(-0.707106781186548,-0.707106781186547,0.));
#6965=DIRECTION('',(0.,-1.,0.));
#6966=DIRECTION('',(0.707106781186548,-0.707106781186548,0.));
#6967=DIRECTION('center_axis',(1.,0.,0.));
#6968=DIRECTION('ref_axis',(0.,-0.707106781186554,0.707106781186541));
#6969=DIRECTION('center_axis',(0.923879532511286,-0.382683432365092,0.));
#6970=DIRECTION('ref_axis',(-0.382683432365092,-0.923879532511286,0.));
#6971=DIRECTION('',(1.,0.,0.));
#6972=DIRECTION('center_axis',(1.,0.,0.));
#6973=DIRECTION('ref_axis',(0.,-0.707106781186554,0.707106781186541));
#6974=DIRECTION('',(1.,0.,0.));
#6975=DIRECTION('center_axis',(0.923879532511283,0.382683432365099,0.));
#6976=DIRECTION('ref_axis',(-0.382683432365099,0.923879532511283,0.));
#6977=DIRECTION('center_axis',(-1.,0.,0.));
#6978=DIRECTION('ref_axis',(0.,-0.707106781186548,-0.707106781186548));
#6979=DIRECTION('',(1.,0.,0.));
#6980=DIRECTION('center_axis',(-0.923879532511283,-0.382683432365099,4.10284931589583E-15));
#6981=DIRECTION('ref_axis',(0.382683432365098,-0.923879532511283,9.90515446280861E-15));
#6982=DIRECTION('',(-1.,0.,0.));
#6983=DIRECTION('center_axis',(-0.923879532511286,0.382683432365092,0.));
#6984=DIRECTION('ref_axis',(0.382683432365091,0.923879532511286,0.));
#6985=DIRECTION('center_axis',(0.,1.,0.));
#6986=DIRECTION('ref_axis',(0.707106781186551,0.,-0.707106781186544));
#6987=DIRECTION('',(0.,1.,0.));
#6988=DIRECTION('center_axis',(-0.382683432365083,-0.92387953251129,0.));
#6989=DIRECTION('ref_axis',(0.923879532511289,-0.382683432365083,0.));
#6990=DIRECTION('',(0.,-1.,0.));
#6991=DIRECTION('center_axis',(0.382683432365097,0.923879532511284,8.49727915508632E-16));
#6992=DIRECTION('ref_axis',(0.923879532511284,-0.382683432365097,2.05142465794791E-15));
#6993=DIRECTION('center_axis',(0.707106781186548,0.707106781186548,0.));
#6994=DIRECTION('ref_axis',(0.499999999999996,-0.500000000000002,-0.707106781186549));
#6995=DIRECTION('',(0.707106781186548,0.707106781186548,0.));
#6996=DIRECTION('center_axis',(-0.92387953251129,-0.382683432365082,0.));
#6997=DIRECTION('ref_axis',(0.382683432365082,-0.92387953251129,0.));
#6998=DIRECTION('',(-0.707106781186548,-0.707106781186548,0.));
#6999=DIRECTION('center_axis',(0.,1.,0.));
#7000=DIRECTION('ref_axis',(0.707106781186548,0.,-0.707106781186548));
#7001=DIRECTION('',(0.,-1.,0.));
#7002=DIRECTION('center_axis',(0.382683432365093,0.923879532511285,0.));
#7003=DIRECTION('ref_axis',(0.923879532511285,-0.382683432365093,0.));
#7004=DIRECTION('',(0.,1.,0.));
#7005=DIRECTION('center_axis',(0.382683432365092,-0.923879532511286,0.));
#7006=DIRECTION('ref_axis',(-0.923879532511286,-0.382683432365092,0.));
#7007=DIRECTION('center_axis',(1.,4.56509835347174E-16,0.));
#7008=DIRECTION('ref_axis',(0.,-0.707106781186551,-0.707106781186544));
#7009=DIRECTION('',(1.,4.56509835347174E-16,0.));
#7010=DIRECTION('center_axis',(-0.923879532511287,-0.38268343236509,0.));
#7011=DIRECTION('ref_axis',(-0.38268343236509,0.923879532511287,0.));
#7012=DIRECTION('',(-1.,-4.56509835347174E-16,0.));
#7013=DIRECTION('center_axis',(0.707106781186548,0.707106781186547,0.));
#7014=DIRECTION('ref_axis',(0.5,-0.5,-0.707106781186547));
#7015=DIRECTION('',(-0.707106781186548,-0.707106781186547,0.));
#7016=DIRECTION('',(0.707106781186548,0.707106781186547,0.));
#7017=DIRECTION('center_axis',(-0.707106781186548,0.707106781186548,0.));
#7018=DIRECTION('ref_axis',(0.5,0.5,-0.707106781186547));
#7019=DIRECTION('',(0.707106781186548,-0.707106781186548,0.));
#7020=DIRECTION('',(-0.707106781186548,0.707106781186548,0.));
#7021=DIRECTION('center_axis',(0.923879532511286,-0.382683432365092,0.));
#7022=DIRECTION('ref_axis',(-0.382683432365091,-0.923879532511286,0.));
#7023=DIRECTION('center_axis',(-1.,0.,0.));
#7024=DIRECTION('ref_axis',(0.,0.707106781186548,-0.707106781186548));
#7025=DIRECTION('',(1.,0.,0.));
#7026=DIRECTION('',(-1.,0.,0.));
#7027=DIRECTION('center_axis',(0.923879532511286,0.382683432365092,0.));
#7028=DIRECTION('ref_axis',(0.382683432365092,-0.923879532511286,0.));
#7029=DIRECTION('center_axis',(0.707106781186548,0.707106781186548,0.));
#7030=DIRECTION('ref_axis',(0.5,-0.5,-0.707106781186547));
#7031=DIRECTION('',(0.707106781186548,0.707106781186548,0.));
#7032=DIRECTION('',(-0.707106781186548,-0.707106781186548,0.));
#7033=DIRECTION('center_axis',(-0.707106781186548,-0.707106781186548,0.));
#7034=DIRECTION('ref_axis',(-0.5,0.5,-0.707106781186547));
#7035=DIRECTION('',(0.707106781186548,0.707106781186548,0.));
#7036=DIRECTION('',(-0.707106781186548,-0.707106781186548,0.));
#7037=DIRECTION('center_axis',(0.382683432365092,0.923879532511286,0.));
#7038=DIRECTION('ref_axis',(0.923879532511286,-0.382683432365091,0.));
#7039=DIRECTION('center_axis',(0.,-1.,0.));
#7040=DIRECTION('ref_axis',(-0.707106781186548,0.,-0.707106781186548));
#7041=DIRECTION('',(0.,1.,0.));
#7042=DIRECTION('',(0.,-1.,0.));
#7043=DIRECTION('center_axis',(-0.382683432365092,0.923879532511286,0.));
#7044=DIRECTION('ref_axis',(0.923879532511286,0.382683432365092,0.));
#7045=DIRECTION('center_axis',(0.707106781186548,-0.707106781186548,0.));
#7046=DIRECTION('ref_axis',(-0.5,-0.5,-0.707106781186547));
#7047=DIRECTION('',(-0.707106781186548,0.707106781186548,0.));
#7048=DIRECTION('',(0.707106781186548,-0.707106781186548,0.));
#7049=DIRECTION('center_axis',(0.707106781186548,-0.707106781186548,0.));
#7050=DIRECTION('ref_axis',(0.,0.,-1.));
#7051=DIRECTION('',(0.,0.,1.));
#7052=DIRECTION('',(0.707106781186548,0.707106781186548,0.));
#7053=DIRECTION('',(0.,0.,-1.));
#7054=DIRECTION('center_axis',(1.,0.,0.));
#7055=DIRECTION('ref_axis',(0.,1.,0.));
#7056=DIRECTION('',(0.,0.,1.));
#7057=DIRECTION('',(0.,1.,0.));
#7058=DIRECTION('center_axis',(0.707106781186548,-0.707106781186548,0.));
#7059=DIRECTION('ref_axis',(0.707106781186548,0.707106781186548,0.));
#7060=DIRECTION('',(0.,0.,1.));
#7061=DIRECTION('',(0.707106781186548,0.707106781186548,0.));
#7062=DIRECTION('center_axis',(4.56509835347174E-16,-1.,0.));
#7063=DIRECTION('ref_axis',(1.,4.56509835347174E-16,0.));
#7064=DIRECTION('',(0.,0.,-1.));
#7065=DIRECTION('',(1.,4.56509835347174E-16,0.));
#7066=DIRECTION('center_axis',(0.707106781186547,-0.707106781186548,0.));
#7067=DIRECTION('ref_axis',(0.,0.,-1.));
#7068=DIRECTION('',(0.,0.,1.));
#7069=DIRECTION('',(0.707106781186548,0.707106781186547,0.));
#7070=DIRECTION('center_axis',(1.,0.,0.));
#7071=DIRECTION('ref_axis',(0.,1.,0.));
#7072=DIRECTION('',(0.,0.,1.));
#7073=DIRECTION('',(0.,1.,0.));
#7074=DIRECTION('center_axis',(0.,0.,1.));
#7075=DIRECTION('ref_axis',(1.,0.,0.));
#7076=DIRECTION('center_axis',(0.707106781186548,-0.707106781186548,0.));
#7077=DIRECTION('ref_axis',(-0.500000000000005,-0.500000000000005,0.707106781186541));
#7078=DIRECTION('center_axis',(0.382683432365092,-0.923879532511286,0.));
#7079=DIRECTION('ref_axis',(-0.923879532511286,-0.382683432365092,0.));
#7080=DIRECTION('',(0.707106781186548,-0.707106781186548,0.));
#7081=DIRECTION('center_axis',(0.,-1.,0.));
#7082=DIRECTION('ref_axis',(-0.707106781186554,0.,0.707106781186541));
#7083=DIRECTION('center_axis',(-0.382683432365092,-0.923879532511286,0.));
#7084=DIRECTION('ref_axis',(-0.923879532511286,0.382683432365092,0.));
#7085=DIRECTION('',(0.,-1.,0.));
#7086=DIRECTION('center_axis',(-0.707106781186548,-0.707106781186548,0.));
#7087=DIRECTION('ref_axis',(-0.500000000000005,0.500000000000005,0.707106781186541));
#7088=DIRECTION('',(-0.707106781186548,-0.707106781186548,0.));
#7089=DIRECTION('center_axis',(-0.707106781186548,0.707106781186548,0.));
#7090=DIRECTION('ref_axis',(0.500000000000005,0.500000000000005,0.707106781186541));
#7091=DIRECTION('center_axis',(-0.382683432365092,0.923879532511286,0.));
#7092=DIRECTION('ref_axis',(0.923879532511286,0.382683432365092,0.));
#7093=DIRECTION('',(-0.707106781186548,0.707106781186548,0.));
#7094=DIRECTION('center_axis',(0.,1.,0.));
#7095=DIRECTION('ref_axis',(0.707106781186554,0.,0.707106781186541));
#7096=DIRECTION('center_axis',(0.382683432365093,0.923879532511285,0.));
#7097=DIRECTION('ref_axis',(0.923879532511285,-0.382683432365093,0.));
#7098=DIRECTION('center_axis',(-0.707106781186548,-0.707106781186547,0.));
#7099=DIRECTION('ref_axis',(0.5,-0.5,0.707106781186547));
#7100=DIRECTION('center_axis',(0.923879532511287,0.38268343236509,0.));
#7101=DIRECTION('ref_axis',(-0.38268343236509,0.923879532511287,0.));
#7102=DIRECTION('center_axis',(1.,4.56509835347174E-16,0.));
#7103=DIRECTION('ref_axis',(0.,-0.707106781186557,0.707106781186538));
#7104=DIRECTION('center_axis',(0.92387953251129,0.382683432365082,0.));
#7105=DIRECTION('ref_axis',(-0.382683432365082,0.92387953251129,0.));
#7106=DIRECTION('center_axis',(0.707106781186548,0.707106781186548,0.));
#7107=DIRECTION('ref_axis',(0.500000000000005,-0.500000000000005,0.707106781186541));
#7108=DIRECTION('center_axis',(0.382683432365087,0.923879532511288,0.));
#7109=DIRECTION('ref_axis',(-0.923879532511288,0.382683432365087,0.));
#7110=DIRECTION('center_axis',(0.,1.,0.));
#7111=DIRECTION('ref_axis',(0.707106781186557,0.,0.707106781186538));
#7112=DIRECTION('center_axis',(0.382683432365097,0.923879532511284,-8.4972791550864E-16));
#7113=DIRECTION('ref_axis',(0.923879532511284,-0.382683432365097,-2.05142465794793E-15));
#7114=DIRECTION('center_axis',(-0.707106781186548,-0.707106781186548,0.));
#7115=DIRECTION('ref_axis',(0.5,-0.5,0.707106781186547));
#7116=DIRECTION('center_axis',(0.,-1.,0.));
#7117=DIRECTION('ref_axis',(1.,0.,0.));
#7118=DIRECTION('',(0.,0.,1.));
#7119=DIRECTION('center_axis',(-0.707106781186548,-0.707106781186548,0.));
#7120=DIRECTION('ref_axis',(0.707106781186548,-0.707106781186548,0.));
#7121=DIRECTION('',(0.,0.,1.));
#7122=DIRECTION('center_axis',(-1.,0.,0.));
#7123=DIRECTION('ref_axis',(0.,-1.,0.));
#7124=DIRECTION('',(0.,0.,1.));
#7125=DIRECTION('center_axis',(-0.707106781186548,0.707106781186548,0.));
#7126=DIRECTION('ref_axis',(-0.707106781186548,-0.707106781186548,0.));
#7127=DIRECTION('',(0.,0.,1.));
#7128=DIRECTION('center_axis',(0.,1.,0.));
#7129=DIRECTION('ref_axis',(-1.,0.,0.));
#7130=DIRECTION('',(0.,0.,1.));
#7131=DIRECTION('center_axis',(0.707106781186548,0.707106781186548,0.));
#7132=DIRECTION('ref_axis',(-0.707106781186548,0.707106781186548,0.));
#8645=CARTESIAN_POINT('',(0.,0.,0.));
#8646=CARTESIAN_POINT('Origin',(-8.5,-49.,85.));
#8647=CARTESIAN_POINT('',(-4.5,-49.,90.));
#8648=CARTESIAN_POINT('',(-8.5,-49.,86.));
#8649=CARTESIAN_POINT('Origin',(-8.5,-49.,90.));
#8650=CARTESIAN_POINT('',(-8.5,-50.,85.));
#8651=CARTESIAN_POINT('Origin',(-8.5,-49.,85.));
#8652=CARTESIAN_POINT('',(-4.5,-50.,89.8989794855664));
#8653=CARTESIAN_POINT('Ctrl Pts',(-8.5,-50.,85.));
#8654=CARTESIAN_POINT('Ctrl Pts',(-7.96337444213282,-50.,85.2683127789336));
#8655=CARTESIAN_POINT('Ctrl Pts',(-7.37146954918018,-50.,85.5644396994907));
#8656=CARTESIAN_POINT('Ctrl Pts',(-6.29356794340685,-50.,86.2912190109971));
#8657=CARTESIAN_POINT('Ctrl Pts',(-5.81057468241034,-50.,86.7263159860593));
#8658=CARTESIAN_POINT('Ctrl Pts',(-5.16020070925815,-50.,87.5716441011679));
#8659=CARTESIAN_POINT('Ctrl Pts',(-4.89013404243441,-50.,88.0621303350776));
#8660=CARTESIAN_POINT('Ctrl Pts',(-4.59098232128521,-50.,88.9247155210796));
#8661=CARTESIAN_POINT('Ctrl Pts',(-4.5,-50.,89.4525943977152));
#8662=CARTESIAN_POINT('Ctrl Pts',(-4.5,-50.,89.8989794855664));
#8663=CARTESIAN_POINT('Origin',(-4.5,-49.,85.));
#8664=CARTESIAN_POINT('Origin',(-8.5,0.,90.));
#8665=CARTESIAN_POINT('',(-4.5,49.,90.));
#8666=CARTESIAN_POINT('',(-8.5,49.,86.));
#8667=CARTESIAN_POINT('Origin',(-8.5,49.,90.));
#8668=CARTESIAN_POINT('',(-8.5,0.,86.));
#8669=CARTESIAN_POINT('',(-4.5,0.,90.));
#8670=CARTESIAN_POINT('Origin',(-8.5,49.,85.));
#8671=CARTESIAN_POINT('',(-4.5,50.,89.8989794855664));
#8672=CARTESIAN_POINT('',(-8.5,50.,85.));
#8673=CARTESIAN_POINT('Ctrl Pts',(-4.5,50.,89.8989794855664));
#8674=CARTESIAN_POINT('Ctrl Pts',(-4.5,50.,89.4525943977152));
#8675=CARTESIAN_POINT('Ctrl Pts',(-4.59098232128521,50.,88.9247155210796));
#8676=CARTESIAN_POINT('Ctrl Pts',(-4.89013404243441,50.,88.0621303350776));
#8677=CARTESIAN_POINT('Ctrl Pts',(-5.16020070925815,50.,87.5716441011679));
#8678=CARTESIAN_POINT('Ctrl Pts',(-5.81057468241034,50.,86.7263159860593));
#8679=CARTESIAN_POINT('Ctrl Pts',(-6.29356794340685,50.,86.2912190109971));
#8680=CARTESIAN_POINT('Ctrl Pts',(-7.37146954918018,50.,85.5644396994907));
#8681=CARTESIAN_POINT('Ctrl Pts',(-7.96337444213282,50.,85.2683127789336));
#8682=CARTESIAN_POINT('Ctrl Pts',(-8.5,50.,85.));
#8683=CARTESIAN_POINT('Origin',(-8.5,49.,85.));
#8684=CARTESIAN_POINT('Origin',(-4.5,49.,85.));
#8685=CARTESIAN_POINT('Origin',(-4.5,0.,102.763485025341));
#8686=CARTESIAN_POINT('',(-4.5,-50.,120.526970050681));
#8687=CARTESIAN_POINT('',(-4.5,-50.,85.));
#8688=CARTESIAN_POINT('',(-4.5,50.,93.7320508075689));
#8689=CARTESIAN_POINT('',(-4.5,46.0011587545003,94.8035370899608));
#8690=CARTESIAN_POINT('',(-4.5,50.,85.));
#8691=CARTESIAN_POINT('Origin',(9.5,49.,85.));
#8692=CARTESIAN_POINT('',(5.5,49.,90.));
#8693=CARTESIAN_POINT('',(9.5,49.,86.));
#8694=CARTESIAN_POINT('Origin',(9.5,49.,90.));
#8695=CARTESIAN_POINT('',(9.5,50.,85.));
#8696=CARTESIAN_POINT('Origin',(9.5,49.,85.));
#8697=CARTESIAN_POINT('',(5.5,50.,89.8989794855664));
#8698=CARTESIAN_POINT('Ctrl Pts',(9.5,50.,85.));
#8699=CARTESIAN_POINT('Ctrl Pts',(8.96337444213282,50.,85.2683127789336));
#8700=CARTESIAN_POINT('Ctrl Pts',(8.37146954918018,50.,85.5644396994907));
#8701=CARTESIAN_POINT('Ctrl Pts',(7.29356794340685,50.,86.2912190109971));
#8702=CARTESIAN_POINT('Ctrl Pts',(6.81057468241033,50.,86.7263159860593));
#8703=CARTESIAN_POINT('Ctrl Pts',(6.16020070925815,50.,87.5716441011679));
#8704=CARTESIAN_POINT('Ctrl Pts',(5.8901340424344,50.,88.0621303350776));
#8705=CARTESIAN_POINT('Ctrl Pts',(5.59098232128521,50.,88.9247155210796));
#8706=CARTESIAN_POINT('Ctrl Pts',(5.5,50.,89.4525943977152));
#8707=CARTESIAN_POINT('Ctrl Pts',(5.5,50.,89.8989794855664));
#8708=CARTESIAN_POINT('Origin',(5.5,49.,85.));
#8709=CARTESIAN_POINT('Origin',(9.5,0.,90.));
#8710=CARTESIAN_POINT('',(5.5,-49.,90.));
#8711=CARTESIAN_POINT('',(9.5,-49.,86.));
#8712=CARTESIAN_POINT('Origin',(9.5,-49.,90.));
#8713=CARTESIAN_POINT('',(9.5,0.,86.));
#8714=CARTESIAN_POINT('',(5.5,0.,90.));
#8715=CARTESIAN_POINT('Origin',(9.5,-49.,85.));
#8716=CARTESIAN_POINT('',(5.5,-50.,89.8989794855664));
#8717=CARTESIAN_POINT('',(9.5,-50.,85.));
#8718=CARTESIAN_POINT('Ctrl Pts',(5.5,-50.,89.8989794855664));
#8719=CARTESIAN_POINT('Ctrl Pts',(5.5,-50.,89.4525943977152));
#8720=CARTESIAN_POINT('Ctrl Pts',(5.59098232128521,-50.,88.9247155210796));
#8721=CARTESIAN_POINT('Ctrl Pts',(5.8901340424344,-50.,88.0621303350776));
#8722=CARTESIAN_POINT('Ctrl Pts',(6.16020070925815,-50.,87.5716441011679));
#8723=CARTESIAN_POINT('Ctrl Pts',(6.81057468241033,-50.,86.7263159860593));
#8724=CARTESIAN_POINT('Ctrl Pts',(7.29356794340685,-50.,86.2912190109971));
#8725=CARTESIAN_POINT('Ctrl Pts',(8.37146954918018,-50.,85.5644396994907));
#8726=CARTESIAN_POINT('Ctrl Pts',(8.96337444213282,-50.,85.2683127789336));
#8727=CARTESIAN_POINT('Ctrl Pts',(9.5,-50.,85.));
#8728=CARTESIAN_POINT('Origin',(9.5,-49.,85.));
#8729=CARTESIAN_POINT('Origin',(5.5,-49.,85.));
#8730=CARTESIAN_POINT('Origin',(5.5,0.,102.763485025341));
#8731=CARTESIAN_POINT('',(5.5,50.,93.7320508075689));
#8732=CARTESIAN_POINT('',(5.5,50.,85.));
#8733=CARTESIAN_POINT('',(5.5,-50.,120.526970050681));
#8734=CARTESIAN_POINT('',(5.5,46.0011587545003,94.8035370899608));
#8735=CARTESIAN_POINT('',(5.5,-50.,85.));
#8736=CARTESIAN_POINT('Origin',(-32.4855257306532,-32.7240321735238,86.));
#8737=CARTESIAN_POINT('',(-29.4855257306532,-32.7240321735238,86.));
#8738=CARTESIAN_POINT('Origin',(-32.4855257306532,-32.7240321735238,86.));
#8739=CARTESIAN_POINT('',(-29.4855257306532,-32.7240321735238,74.));
#8740=CARTESIAN_POINT('',(-29.4855257306532,-32.7240321735238,86.));
#8741=CARTESIAN_POINT('Origin',(-32.4855257306532,-32.7240321735238,74.));
#8742=CARTESIAN_POINT('Origin',(32.5144742693468,32.2759678264762,86.));
#8743=CARTESIAN_POINT('',(35.5144742693468,32.2759678264762,86.));
#8744=CARTESIAN_POINT('Origin',(32.5144742693468,32.2759678264762,86.));
#8745=CARTESIAN_POINT('',(35.5144742693468,32.2759678264762,74.));
#8746=CARTESIAN_POINT('',(35.5144742693468,32.2759678264762,86.));
#8747=CARTESIAN_POINT('Origin',(32.5144742693468,32.2759678264762,74.));
#8748=CARTESIAN_POINT('Origin',(-32.4855257306532,32.2759678264762,86.));
#8749=CARTESIAN_POINT('',(-29.4855257306532,32.2759678264762,86.));
#8750=CARTESIAN_POINT('Origin',(-32.4855257306532,32.2759678264762,86.));
#8751=CARTESIAN_POINT('',(-29.4855257306532,32.2759678264762,74.));
#8752=CARTESIAN_POINT('',(-29.4855257306532,32.2759678264762,86.));
#8753=CARTESIAN_POINT('Origin',(-32.4855257306532,32.2759678264762,74.));
#8754=CARTESIAN_POINT('Origin',(32.5144742693468,-7.72403217352376,86.));
#8755=CARTESIAN_POINT('',(35.5144742693468,-7.72403217352376,86.));
#8756=CARTESIAN_POINT('Origin',(32.5144742693468,-7.72403217352376,86.));
#8757=CARTESIAN_POINT('',(35.5144742693468,-7.72403217352376,74.));
#8758=CARTESIAN_POINT('',(35.5144742693468,-7.72403217352376,86.));
#8759=CARTESIAN_POINT('Origin',(32.5144742693468,-7.72403217352376,74.));
#8760=CARTESIAN_POINT('Origin',(0.499999999999998,50.,93.7320508075689));
#8761=CARTESIAN_POINT('',(0.499999999999998,-50.,120.526970050681));
#8762=CARTESIAN_POINT('',(0.499999999999998,50.,93.7320508075689));
#8763=CARTESIAN_POINT('Origin',(22.5,49.,85.));
#8764=CARTESIAN_POINT('',(-45.,50.,85.));
#8765=CARTESIAN_POINT('',(22.5,50.,85.));
#8766=CARTESIAN_POINT('',(-44.5857864376269,49.,86.));
#8767=CARTESIAN_POINT('Origin',(-44.5857864376269,49.,85.));
#8768=CARTESIAN_POINT('',(22.5,49.,86.));
#8769=CARTESIAN_POINT('Origin',(22.5,49.,85.));
#8770=CARTESIAN_POINT('',(44.5857864376269,49.,86.));
#8771=CARTESIAN_POINT('',(22.5,49.,86.));
#8772=CARTESIAN_POINT('',(45.,50.,85.));
#8773=CARTESIAN_POINT('Origin',(44.5857864376269,49.,85.));
#8774=CARTESIAN_POINT('',(22.5,50.,85.));
#8775=CARTESIAN_POINT('Origin',(0.,0.,86.));
#8776=CARTESIAN_POINT('',(-49.,44.5857864376269,86.));
#8777=CARTESIAN_POINT('',(-45.5428932188135,48.0428932188135,86.));
#8778=CARTESIAN_POINT('',(-49.,-44.5857864376269,86.));
#8779=CARTESIAN_POINT('',(-49.,22.5,86.));
#8780=CARTESIAN_POINT('',(-44.5857864376269,-49.,86.));
#8781=CARTESIAN_POINT('',(-48.0428932188135,-45.5428932188135,86.));
#8782=CARTESIAN_POINT('',(-22.5,-49.,86.));
#8783=CARTESIAN_POINT('Origin',(0.,0.,86.));
#8784=CARTESIAN_POINT('',(15.5857864376269,-49.,86.));
#8785=CARTESIAN_POINT('',(-22.5,-49.,86.));
#8786=CARTESIAN_POINT('',(20.,-44.5857864376269,86.));
#8787=CARTESIAN_POINT('',(25.0428932188134,-39.5428932188134,86.));
#8788=CARTESIAN_POINT('',(20.,-30.8578643762691,86.));
#8789=CARTESIAN_POINT('',(20.,-25.,86.));
#8790=CARTESIAN_POINT('',(30.857864376269,-20.,86.));
#8791=CARTESIAN_POINT('',(22.860912703474,-27.9969516727951,86.));
#8792=CARTESIAN_POINT('',(44.5857864376269,-20.,86.));
#8793=CARTESIAN_POINT('',(15.6360389693211,-20.,86.));
#8794=CARTESIAN_POINT('',(49.,-15.5857864376269,86.));
#8795=CARTESIAN_POINT('',(39.5428932188134,-25.0428932188135,86.));
#8796=CARTESIAN_POINT('',(49.,44.5857864376269,86.));
#8797=CARTESIAN_POINT('',(49.,-10.5,86.));
#8798=CARTESIAN_POINT('',(48.0428932188135,45.5428932188135,86.));
#8799=CARTESIAN_POINT('Origin',(-22.5,-49.,85.));
#8800=CARTESIAN_POINT('',(-45.,-50.,85.));
#8801=CARTESIAN_POINT('Origin',(-44.5857864376269,-49.,85.));
#8802=CARTESIAN_POINT('',(-22.5,-50.,85.));
#8803=CARTESIAN_POINT('Origin',(-22.5,-49.,85.));
#8804=CARTESIAN_POINT('',(16.,-50.,85.));
#8805=CARTESIAN_POINT('',(-22.5,-50.,85.));
#8806=CARTESIAN_POINT('Origin',(15.5857864376269,-49.,85.));
#8807=CARTESIAN_POINT('Origin',(-22.5,-49.,75.));
#8808=CARTESIAN_POINT('',(-44.5857864376269,-49.,74.));
#8809=CARTESIAN_POINT('',(15.5857864376269,-49.,74.));
#8810=CARTESIAN_POINT('',(-22.5,-49.,74.));
#8811=CARTESIAN_POINT('',(16.,-50.,75.));
#8812=CARTESIAN_POINT('Origin',(15.5857864376269,-49.,75.));
#8813=CARTESIAN_POINT('',(-45.,-50.,75.));
#8814=CARTESIAN_POINT('',(-22.5,-50.,75.));
#8815=CARTESIAN_POINT('Origin',(-44.5857864376269,-49.,75.));
#8816=CARTESIAN_POINT('Origin',(20.,-25.,75.));
#8817=CARTESIAN_POINT('',(20.,-44.5857864376269,74.));
#8818=CARTESIAN_POINT('',(20.,-30.8578643762691,74.));
#8819=CARTESIAN_POINT('',(20.,-25.,74.));
#8820=CARTESIAN_POINT('',(21.,-31.2720779386421,75.));
#8821=CARTESIAN_POINT('Origin',(20.,-30.8578643762691,75.));
#8822=CARTESIAN_POINT('',(21.,-45.,75.));
#8823=CARTESIAN_POINT('',(21.,-25.,75.));
#8824=CARTESIAN_POINT('Origin',(20.,-44.5857864376269,75.));
#8825=CARTESIAN_POINT('Origin',(22.860912703474,-27.9969516727951,75.));
#8826=CARTESIAN_POINT('',(30.857864376269,-20.,74.));
#8827=CARTESIAN_POINT('',(22.860912703474,-27.9969516727951,74.));
#8828=CARTESIAN_POINT('',(31.2720779386421,-21.,75.));
#8829=CARTESIAN_POINT('Origin',(30.857864376269,-20.,75.));
#8830=CARTESIAN_POINT('',(23.5680194846605,-28.7040584539816,75.));
#8831=CARTESIAN_POINT('Origin',(49.,-10.5,75.));
#8832=CARTESIAN_POINT('',(50.,45.,75.));
#8833=CARTESIAN_POINT('',(50.,-16.,75.));
#8834=CARTESIAN_POINT('',(50.,-10.5,75.));
#8835=CARTESIAN_POINT('',(49.,-15.5857864376269,74.));
#8836=CARTESIAN_POINT('Origin',(49.,-15.5857864376269,75.));
#8837=CARTESIAN_POINT('',(49.,44.5857864376269,74.));
#8838=CARTESIAN_POINT('',(49.,-10.5,74.));
#8839=CARTESIAN_POINT('Origin',(49.,44.5857864376269,75.));
#8840=CARTESIAN_POINT('Origin',(15.6360389693211,-20.,75.));
#8841=CARTESIAN_POINT('',(44.5857864376269,-20.,74.));
#8842=CARTESIAN_POINT('',(15.6360389693211,-20.,74.));
#8843=CARTESIAN_POINT('',(45.,-21.,75.));
#8844=CARTESIAN_POINT('Origin',(44.5857864376269,-20.,75.));
#8845=CARTESIAN_POINT('',(15.6360389693211,-21.,75.));
#8846=CARTESIAN_POINT('Origin',(39.5428932188134,-25.0428932188135,75.));
#8847=CARTESIAN_POINT('',(40.25,-25.75,75.));
#8848=CARTESIAN_POINT('',(39.5428932188134,-25.0428932188135,74.));
#8849=CARTESIAN_POINT('Origin',(48.0428932188135,45.5428932188135,75.));
#8850=CARTESIAN_POINT('',(45.,50.,75.));
#8851=CARTESIAN_POINT('',(48.75,46.25,75.));
#8852=CARTESIAN_POINT('',(44.5857864376269,49.,74.));
#8853=CARTESIAN_POINT('',(48.0428932188135,45.5428932188135,74.));
#8854=CARTESIAN_POINT('Origin',(44.5857864376269,49.,75.));
#8855=CARTESIAN_POINT('Origin',(22.5,49.,75.));
#8856=CARTESIAN_POINT('',(-45.,50.,75.));
#8857=CARTESIAN_POINT('',(22.5,50.,75.));
#8858=CARTESIAN_POINT('',(-44.5857864376269,49.,74.));
#8859=CARTESIAN_POINT('',(22.5,49.,74.));
#8860=CARTESIAN_POINT('Origin',(-44.5857864376269,49.,75.));
#8861=CARTESIAN_POINT('Origin',(25.0428932188134,-39.5428932188134,75.));
#8862=CARTESIAN_POINT('',(25.0428932188134,-39.5428932188134,74.));
#8863=CARTESIAN_POINT('',(25.75,-40.25,75.));
#8864=CARTESIAN_POINT('Origin',(-45.5428932188135,48.0428932188135,75.));
#8865=CARTESIAN_POINT('',(-50.,45.,75.));
#8866=CARTESIAN_POINT('',(-46.25,48.75,75.));
#8867=CARTESIAN_POINT('',(-49.,44.5857864376269,74.));
#8868=CARTESIAN_POINT('',(-45.5428932188135,48.0428932188135,74.));
#8869=CARTESIAN_POINT('Origin',(-49.,44.5857864376269,75.));
#8870=CARTESIAN_POINT('Origin',(-49.,22.5,75.));
#8871=CARTESIAN_POINT('',(-50.,-45.,75.));
#8872=CARTESIAN_POINT('',(-50.,22.5,75.));
#8873=CARTESIAN_POINT('',(-49.,-44.5857864376269,74.));
#8874=CARTESIAN_POINT('',(-49.,22.5,74.));
#8875=CARTESIAN_POINT('Origin',(-49.,-44.5857864376269,75.));
#8876=CARTESIAN_POINT('Origin',(-48.0428932188135,-45.5428932188135,75.));
#8877=CARTESIAN_POINT('',(-48.75,-46.25,75.));
#8878=CARTESIAN_POINT('',(-48.0428932188135,-45.5428932188135,74.));
#8879=CARTESIAN_POINT('Origin',(18.5,-47.5,74.));
#8880=CARTESIAN_POINT('',(21.,-45.,85.));
#8881=CARTESIAN_POINT('',(21.,-45.,74.));
#8882=CARTESIAN_POINT('',(25.75,-40.25,85.));
#8883=CARTESIAN_POINT('',(16.,-50.,74.));
#8884=CARTESIAN_POINT('Origin',(21.,-50.,74.));
#8885=CARTESIAN_POINT('',(21.,-31.2720779386421,85.));
#8886=CARTESIAN_POINT('',(21.,-31.2720779386421,74.));
#8887=CARTESIAN_POINT('',(21.,-25.,85.));
#8888=CARTESIAN_POINT('Origin',(21.,-31.2720779386421,74.));
#8889=CARTESIAN_POINT('',(31.2720779386421,-21.,85.));
#8890=CARTESIAN_POINT('',(31.2720779386421,-21.,74.));
#8891=CARTESIAN_POINT('',(23.5680194846605,-28.7040584539816,85.));
#8892=CARTESIAN_POINT('Origin',(31.2720779386421,-21.,74.));
#8893=CARTESIAN_POINT('',(45.,-21.,85.));
#8894=CARTESIAN_POINT('',(45.,-21.,74.));
#8895=CARTESIAN_POINT('',(15.6360389693211,-21.,85.));
#8896=CARTESIAN_POINT('Origin',(47.5,-18.5,74.));
#8897=CARTESIAN_POINT('',(50.,-16.,85.));
#8898=CARTESIAN_POINT('',(50.,-16.,74.));
#8899=CARTESIAN_POINT('',(40.25,-25.75,85.));
#8900=CARTESIAN_POINT('Origin',(50.,-21.,74.));
#8901=CARTESIAN_POINT('',(50.,45.,85.));
#8902=CARTESIAN_POINT('',(50.,45.,74.));
#8903=CARTESIAN_POINT('',(50.,-10.5,85.));
#8904=CARTESIAN_POINT('Origin',(0.,0.,74.));
#8905=CARTESIAN_POINT('Origin',(-48.0428932188135,-45.5428932188135,85.));
#8906=CARTESIAN_POINT('',(-50.,-45.,85.));
#8907=CARTESIAN_POINT('Origin',(-49.,-44.5857864376269,85.));
#8908=CARTESIAN_POINT('',(-48.75,-46.25,85.));
#8909=CARTESIAN_POINT('Origin',(-49.,22.5,85.));
#8910=CARTESIAN_POINT('',(-50.,45.,85.));
#8911=CARTESIAN_POINT('Origin',(-49.,44.5857864376269,85.));
#8912=CARTESIAN_POINT('',(-50.,22.5,85.));
#8913=CARTESIAN_POINT('Origin',(-45.5428932188135,48.0428932188135,85.));
#8914=CARTESIAN_POINT('',(-46.25,48.75,85.));
#8915=CARTESIAN_POINT('Origin',(48.0428932188135,45.5428932188135,85.));
#8916=CARTESIAN_POINT('Origin',(49.,44.5857864376269,85.));
#8917=CARTESIAN_POINT('',(48.75,46.25,85.));
#8918=CARTESIAN_POINT('Origin',(49.,-10.5,85.));
#8919=CARTESIAN_POINT('Origin',(49.,-15.5857864376269,85.));
#8920=CARTESIAN_POINT('Origin',(39.5428932188134,-25.0428932188135,85.));
#8921=CARTESIAN_POINT('Origin',(44.5857864376269,-20.,85.));
#8922=CARTESIAN_POINT('Origin',(15.6360389693211,-20.,85.));
#8923=CARTESIAN_POINT('Origin',(30.857864376269,-20.,85.));
#8924=CARTESIAN_POINT('Origin',(22.860912703474,-27.9969516727951,85.));
#8925=CARTESIAN_POINT('Origin',(20.,-30.8578643762691,85.));
#8926=CARTESIAN_POINT('Origin',(20.,-25.,85.));
#8927=CARTESIAN_POINT('Origin',(20.,-44.5857864376269,85.));
#8928=CARTESIAN_POINT('Origin',(25.0428932188134,-39.5428932188134,85.));
#8929=CARTESIAN_POINT('Origin',(-45.,-50.,74.));
#8930=CARTESIAN_POINT('',(-45.,-50.,74.));
#8931=CARTESIAN_POINT('Origin',(-50.,-45.,74.));
#8932=CARTESIAN_POINT('',(-50.,-45.,74.));
#8933=CARTESIAN_POINT('Origin',(-50.,45.,74.));
#8934=CARTESIAN_POINT('',(-50.,45.,74.));
#8935=CARTESIAN_POINT('Origin',(-45.,50.,74.));
#8936=CARTESIAN_POINT('',(-45.,50.,74.));
#8937=CARTESIAN_POINT('Origin',(45.,50.,74.));
#8938=CARTESIAN_POINT('',(45.,50.,74.));
#8939=CARTESIAN_POINT('Origin',(50.,45.,74.));
#10111=UNCERTAINTY_MEASURE_WITH_UNIT(LENGTH_MEASURE(0.01),#10132,
'DISTANCE_ACCURACY_VALUE',
'Maximum model space distance between geometric entities at asserted c
onnectivities');
#10119=UNCERTAINTY_MEASURE_WITH_UNIT(LENGTH_MEASURE(0.01),#10132,
'DISTANCE_ACCURACY_VALUE',
'Maximum model space distance between geometric entities at asserted c
onnectivities');
#10123=(
GEOMETRIC_REPRESENTATION_CONTEXT(3)
GLOBAL_UNCERTAINTY_ASSIGNED_CONTEXT((#10111))
GLOBAL_UNIT_ASSIGNED_CONTEXT((#10132,#10134,#10135))
REPRESENTATION_CONTEXT('','3D')
);
#10131=(
GEOMETRIC_REPRESENTATION_CONTEXT(3)
GLOBAL_UNCERTAINTY_ASSIGNED_CONTEXT((#10119))
GLOBAL_UNIT_ASSIGNED_CONTEXT((#10132,#10134,#10135))
REPRESENTATION_CONTEXT('','3D')
);
#10132=(
LENGTH_UNIT()
NAMED_UNIT(*)
SI_UNIT(.MILLI.,.METRE.)
);
#10134=(
NAMED_UNIT(*)
PLANE_ANGLE_UNIT()
SI_UNIT($,.RADIAN.)
);
#10135=(
NAMED_UNIT(*)
SI_UNIT($,.STERADIAN.)
SOLID_ANGLE_UNIT()
);
#10139=SHAPE_DEFINITION_REPRESENTATION(#10150,#10171);
#10150=PRODUCT_DEFINITION_SHAPE('',$,#10183);
#10171=SHAPE_REPRESENTATION('',(#6074),#10123);
#10179=PRODUCT_DEFINITION_CONTEXT('part definition',#10214,'design');
#10183=PRODUCT_DEFINITION('Top_Block','Top_Block',#10194,#10179);
#10194=PRODUCT_DEFINITION_FORMATION('',$,#10219);
#10214=APPLICATION_CONTEXT(
'Core Data for Automotive Mechanical Design Process');
#10215=PRODUCT_CONTEXT('part definition',#10214,'mechanical');
#10219=PRODUCT('Top_Block','Top_Block',$,(#10215));
#10241=COLOUR_RGB('Dark Blue',0.08,0.2,0.34);
#10242=FILL_AREA_STYLE_COLOUR('',#10241);
#10243=FILL_AREA_STYLE('',(#10242));
#10244=SURFACE_STYLE_FILL_AREA(#10243);
#10245=SURFACE_SIDE_STYLE('',(#10244));
#10246=SURFACE_STYLE_USAGE(.BOTH.,#10245);
#10247=PRESENTATION_STYLE_ASSIGNMENT((#10246));
ENDSEC;
END-ISO-10303-21;
